ISO-10303-21;
HEADER;
FILE_DESCRIPTION (('STEP AP214'),
    '1' );
FILE_NAME ('hex flange nut gradea_iso_ISO - 4161 - M10 - N.step',
    '2026-10-25T05:52:03',
    ( '' ),
    ( '' ),
    'SwSTEP 2.0',
    'SolidWorks 2026',
    '' );
FILE_SCHEMA (( 'AUTOMOTIVE_DESIGN' ));
ENDSEC;

DATA;
#34=DIRECTION ( 'NONE',  ( 0.000000000000000000, 0.000000000000000000, 1.000000000000000000 ) ) ;
#38=CARTESIAN_POINT ( 'NONE',  ( -7.500000000000007105, 4.330127018922190096, -7.564335161054478895 ) ) ;
#40=CARTESIAN_POINT ( 'NONE',  ( 3.749999999999999112, -6.495190528383302464, -6.991905250253757309 ) ) ;
#54=CARTESIAN_POINT ( 'NONE',  ( 4.336808689942017736E-16, 8.660254037844390851, -1.000000000000000888 ) ) ;
#126=FACE_OUTER_BOUND ( 'NONE', #12177, .T. ) ;
#201=CARTESIAN_POINT ( 'NONE',  ( -6.901579824520442941, 4.675625068323816080, -0.7022220667781327030 ) ) ;
#215=CARTESIAN_POINT ( 'NONE',  ( -5.276498195231978272, 6.073236878017963747, -7.633618187056680604 ) ) ;
#242=APPLICATION_CONTEXT ( 'automotive_design' ) ;
#249=PRODUCT_CONTEXT ( 'NONE', #29797, 'mechanical' ) ;
#274=EDGE_LOOP ( 'NONE', ( #55468, #62906 ) ) ;
#352=CARTESIAN_POINT ( 'NONE',  ( -7.808218555861945021, 4.508077085120198113, -7.999534413642733988 ) ) ;
#451=FACE_OUTER_BOUND ( 'NONE', #62489, .T. ) ;
#530=CARTESIAN_POINT ( 'NONE',  ( -2.325424218463065351, 7.317669739334662360, -7.030005583190789054 ) ) ;
#543=ORIENTED_EDGE ( 'NONE', *, *, #44898, .F. ) ;
#576=CARTESIAN_POINT ( 'NONE',  ( -7.894706624614703294, -0.7534108004380160040, -7.590222617908770175 ) ) ;
#668=CARTESIAN_POINT ( 'NONE',  ( 6.874999999999999112, 4.690970937165706900, -7.298562697733104621 ) ) ;
#727=VERTEX_POINT ( 'NONE', #55274 ) ;
#749=CARTESIAN_POINT ( 'NONE',  ( -7.500000000000000888, -3.608439182435167591, -7.298562697733108173 ) ) ;
#770=CARTESIAN_POINT ( 'NONE',  ( 1.211595439868046853, -7.960739084487661543, -0.4504974108212073114 ) ) ;
#824=CARTESIAN_POINT ( 'NONE',  ( 6.658902113225075858, 5.287118297641098863, -7.776713651267108673 ) ) ;
#832=ADVANCED_FACE ( 'NONE', ( #17290 ), #62370, .T. ) ;
#1099=CARTESIAN_POINT ( 'NONE',  ( -6.523606932383669843, -4.893847819345372940, -7.213065638944913260 ) ) ;
#1118=VECTOR ( 'NONE', #28038, 1000.000000000000000 ) ;
#1133=CARTESIAN_POINT ( 'NONE',  ( 0.000000000000000000, 0.000000000000000000, 0.000000000000000000 ) ) ;
#1228=CARTESIAN_POINT ( 'NONE',  ( -7.500000000000000000, -3.160302461882432024, -7.231849989190475725 ) ) ;
#1265=EDGE_CURVE ( 'NONE', #38994, #15732, #40055, .T. ) ;
#1318=CARTESIAN_POINT ( 'NONE',  ( 4.599534470797546959, -6.460478697736932396, -7.590212325761396706 ) ) ;
#1322=CARTESIAN_POINT ( 'NONE',  ( 3.749999999999998224, 6.495190528383290918, -6.991905250253753756 ) ) ;
#1330=AXIS2_PLACEMENT_3D ( 'NONE', #24006, #58732, #21415 ) ;
#1407=CYLINDRICAL_SURFACE ( 'NONE', #30891, 4.250000000000000000 ) ;
#1472=CARTESIAN_POINT ( 'NONE',  ( 7.500000000000000000, -3.988190556646209028, -0.8526458641284331286 ) ) ;
#1507=VERTEX_POINT ( 'NONE', #19088 ) ;
#1592=CONICAL_SURFACE ( 'NONE', #39562, 7.500000000000001776, 0.8594454914424796144 ) ;
#1610=PLANE ( 'NONE',  #61219 ) ;
#1627=CARTESIAN_POINT ( 'NONE',  ( 2.558993250143296372, -7.638875775590942219, -7.593821156097518177 ) ) ;
#1699=CYLINDRICAL_SURFACE ( 'NONE', #1770, 4.250000000000000000 ) ;
#1713=ADVANCED_FACE ( 'NONE', ( #56833 ), #54171, .T. ) ;
#1729=CARTESIAN_POINT ( 'NONE',  ( 7.894787914004607998, -0.7647108141804126458, -7.591390474663421095 ) ) ;
#1733=CARTESIAN_POINT ( 'NONE',  ( -5.335963852939856089, -6.035591050534137025, -7.593821156097342318 ) ) ;
#1747=CARTESIAN_POINT ( 'NONE',  ( 7.499999999999999112, 4.652409454067514716, -7.929128589908465585 ) ) ;
#1770=AXIS2_PLACEMENT_3D ( 'NONE', #29980, #60552, #44774 ) ;
#1785=ORIENTED_EDGE ( 'NONE', *, *, #19975, .F. ) ;
#1794=CARTESIAN_POINT ( 'NONE',  ( 7.500000000000001776, 0.000000000000000000, 0.000000000000000000 ) ) ;
#1892=ORIENTED_EDGE ( 'NONE', *, *, #62648, .T. ) ;
#1959=CARTESIAN_POINT ( 'NONE',  ( 7.500000000000000888, 3.639598441879751345, -0.7155132341745285007 ) ) ;
#1987=EDGE_CURVE ( 'NONE', #29821, #727, #46303, .T. ) ;
#2047=DIRECTION ( 'NONE',  ( 0.8191520442889907994, 0.000000000000000000, 0.5735764363510474917 ) ) ;
#2051=CARTESIAN_POINT ( 'NONE',  ( -0.6169862416623524970, -8.783631307150855605, -7.913704048099795330 ) ) ;
#2157=ORIENTED_EDGE ( 'NONE', *, *, #39804, .T. ) ;
#2229=AXIS2_PLACEMENT_3D ( 'NONE', #52684, #57525, #63602 ) ;
#2262=CARTESIAN_POINT ( 'NONE',  ( -7.499999999999999112, 0.3744244963005040061, 1.590163186312071526E-15 ) ) ;
#2340=CARTESIAN_POINT ( 'NONE',  ( 6.902527771671632451, 4.675077770780898589, -0.7026937717022819774 ) ) ;
#2418=EDGE_CURVE ( 'NONE', #23656, #50923, #19369, .T. ) ;
#2658=FACE_OUTER_BOUND ( 'NONE', #50703, .T. ) ;
#2665=CARTESIAN_POINT ( 'NONE',  ( 0.000000000000000000, 0.000000000000000000, -9.974600000000000577 ) ) ;
#2685=DIRECTION ( 'NONE',  ( 0.000000000000000000, 0.000000000000000000, 1.000000000000000000 ) ) ;
#2705=CARTESIAN_POINT ( 'NONE',  ( 7.914973979435151463, 3.817460047930444134, -7.907502498112419786 ) ) ;
#2739=ORIENTED_EDGE ( 'NONE', *, *, #44055, .F. ) ;
#2827=DIRECTION ( 'NONE',  ( 0.000000000000000000, 0.000000000000000000, -1.000000000000000000 ) ) ;
#2890=CARTESIAN_POINT ( 'NONE',  ( -7.500000000000000000, 0.7513028741560130452, -0.02472015219302865774 ) ) ;
#2893=CARTESIAN_POINT ( 'NONE',  ( 7.808623696107353851, 4.508310992947591522, -7.999704684617483963 ) ) ;
#2956=AXIS2_PLACEMENT_3D ( 'NONE', #15838, #36406, #16471 ) ;
#3019=PLANE ( 'NONE',  #29643 ) ;
#3030=CARTESIAN_POINT ( 'NONE',  ( 7.894787914004607998, 0.7661396099416312166, -7.591390474663430865 ) ) ;
#3036=ORIENTED_EDGE ( 'NONE', *, *, #29373, .T. ) ;
#3044=EDGE_LOOP ( 'NONE', ( #48836, #28789, #53241 ) ) ;
#3048=AXIS2_PLACEMENT_3D ( 'NONE', #19419, #24888, #38709 ) ;
#3090=DIRECTION ( 'NONE',  ( -1.000000000000000000, 0.000000000000000000, 0.000000000000000000 ) ) ;
#3096=CIRCLE ( 'NONE', #24648, 4.250000000000000000 ) ;
#3116=DIRECTION ( 'NONE',  ( -0.000000000000000000, -0.000000000000000000, 1.000000000000000000 ) ) ;
#3146=DIRECTION ( 'NONE',  ( 0.000000000000000000, 0.000000000000000000, 1.000000000000000000 ) ) ;
#3168=CARTESIAN_POINT ( 'NONE',  ( -7.922281120364393914, -4.573931137438277617, -8.047472243342932430 ) ) ;
#3236=EDGE_CURVE ( 'NONE', #13010, #29821, #22475, .T. ) ;
#3299=DIRECTION ( 'NONE',  ( 0.8660254037844382635, 0.5000000000000004441, 0.000000000000000000 ) ) ;
#3372=ORIENTED_EDGE ( 'NONE', *, *, #49435, .T. ) ;
#3756=VERTEX_POINT ( 'NONE', #41479 ) ;
#3819=DIRECTION ( 'NONE',  ( -0.8660254037844382635, -0.5000000000000004441, 0.000000000000000000 ) ) ;
#3892=CARTESIAN_POINT ( 'NONE',  ( -7.914984360234579519, 3.818534719232089980, -7.907701344400639876 ) ) ;
#3907=CARTESIAN_POINT ( 'NONE',  ( 3.288228914120474133, -7.217643567644815406, -7.591235721156641247 ) ) ;
#3909=AXIS2_PLACEMENT_3D ( 'NONE', #38429, #62589, #42632 ) ;
#3953=DIRECTION ( 'NONE',  ( -1.000000000000000000, 0.000000000000000000, 0.000000000000000000 ) ) ;
#3955=VECTOR ( 'NONE', #24371, 1000.000000000000000 ) ;
#3968=DIRECTION ( 'NONE',  ( -1.000000000000000000, 0.000000000000000000, 0.000000000000000000 ) ) ;
#3983=CARTESIAN_POINT ( 'NONE',  ( 3.750000000000004441, -6.495190528383289141, 0.000000000000000000 ) ) ;
#4051=EDGE_LOOP ( 'NONE', ( #543, #39844, #14713 ) ) ;
#4062=DIRECTION ( 'NONE',  ( -0.000000000000000000, -0.000000000000000000, 1.000000000000000000 ) ) ;
#4076=CARTESIAN_POINT ( 'NONE',  ( -5.047120108843199837, 5.746297884371392328, -0.1007566405101777279 ) ) ;
#4091=CARTESIAN_POINT ( 'NONE',  ( -1.305263714129178521, 8.377797850839286298, -7.792447862505335721 ) ) ;
#4101=ADVANCED_FACE ( 'NONE', ( #8992 ), #37608, .T. ) ;
#4112=ORIENTED_EDGE ( 'NONE', *, *, #40875, .F. ) ;
#4259=CARTESIAN_POINT ( 'NONE',  ( 0.000000000000000000, 0.000000000000000000, -9.974600000000000577 ) ) ;
#4288=ORIENTED_EDGE ( 'NONE', *, *, #9399, .F. ) ;
#4347=EDGE_LOOP ( 'NONE', ( #43672, #54574, #61495, #61330, #10180, #1892, #43428 ) ) ;
#4353=ORIENTED_EDGE ( 'NONE', *, *, #25660, .T. ) ;
#4419=DIRECTION ( 'NONE',  ( 0.000000000000000000, 0.000000000000000000, 1.000000000000000000 ) ) ;
#4575=ORIENTED_EDGE ( 'NONE', *, *, #26301, .F. ) ;
#4652=DIRECTION ( 'NONE',  ( 1.000000000000000000, 0.000000000000000000, 0.000000000000000000 ) ) ;
#4746=CARTESIAN_POINT ( 'NONE',  ( -7.894955577759523280, 1.603085139988202901, -7.593799241562120272 ) ) ;
#4816=CIRCLE ( 'NONE', #6856, 4.250000000000000000 ) ;
#4851=VERTEX_POINT ( 'NONE', #19825 ) ;
#4882=LINE ( 'NONE', #58910, #22508 ) ;
#4969=ORIENTED_EDGE ( 'NONE', *, *, #42806, .T. ) ;
#4973=VERTEX_POINT ( 'NONE', #40714 ) ;
#5010=CARTESIAN_POINT ( 'NONE',  ( -7.914973979435149687, -3.817460047930451239, -7.907502498112421563 ) ) ;
#5025=CARTESIAN_POINT ( 'NONE',  ( -2.352174619740013739, 7.302225387956623237, -7.450218641348505422 ) ) ;
#5026=CARTESIAN_POINT ( 'NONE',  ( -5.276765049035075705, 6.073111908730296271, -7.634085501268424778 ) ) ;
#5068=CARTESIAN_POINT ( 'NONE',  ( -7.922811899608408481, -4.628803996615321381, -8.057669882367649805 ) ) ;
#5083=MECHANICAL_DESIGN_GEOMETRIC_PRESENTATION_REPRESENTATION('',(#31814),#11284);
#5143=CARTESIAN_POINT ( 'NONE',  ( -3.093157300003891663, -6.874418838041293611, -6.051203375184721622E-15 ) ) ;
#5171=CARTESIAN_POINT ( 'NONE',  ( 0.6249999999999994449, -8.299410119600885594, -7.298562697733110838 ) ) ;
#5182=EDGE_CURVE ( 'NONE', #15732, #14179, #58448, .T. ) ;
#5262=ADVANCED_FACE ( 'NONE', ( #56806 ), #20206, .T. ) ;
#5263=CARTESIAN_POINT ( 'NONE',  ( -7.500000000000000000, -4.330127018922198090, -7.422398894150034288 ) ) ;
#5391=CARTESIAN_POINT ( 'NONE',  ( -7.500000000000000000, 1.644753667986373458, -7.029983668655349405 ) ) ;
#5485=EDGE_CURVE ( 'NONE', #53762, #22221, #7088, .T. ) ;
#5514=VECTOR ( 'NONE', #57229, 1000.000000000000114 ) ;
#5569=DIRECTION ( 'NONE',  ( 0.000000000000000000, 0.000000000000000000, 1.000000000000000000 ) ) ;
#5598=CARTESIAN_POINT ( 'NONE',  ( 6.293430271071537518, -5.026740376715104652, -0.4524126574264552558 ) ) ;
#5798=CARTESIAN_POINT ( 'NONE',  ( 6.250000000000000888, 5.051814855409225480, -7.198902722707425816 ) ) ;
#5801=CARTESIAN_POINT ( 'NONE',  ( 7.499999999999999112, 2.575910028905302074, -0.3641256808890108720 ) ) ;
#5823=EDGE_CURVE ( 'NONE', #49290, #19824, #4816, .T. ) ;
#5910=FACE_OUTER_BOUND ( 'NONE', #10291, .T. ) ;
#5923=CARTESIAN_POINT ( 'NONE',  ( 7.499999999999999112, 3.105728215500122680, -7.659336188854854122 ) ) ;
#5989=EDGE_CURVE ( 'NONE', #57220, #57225, #52079, .T. ) ;
#6018=ORIENTED_EDGE ( 'NONE', *, *, #18800, .T. ) ;
#6043=CARTESIAN_POINT ( 'NONE',  ( -2.352990130084580066E-16, 8.660254037844390851, -10.00000000000000000 ) ) ;
#6130=CARTESIAN_POINT ( 'NONE',  ( 7.500000000000001776, 0.000000000000000000, 0.000000000000000000 ) ) ;
#6156=ORIENTED_EDGE ( 'NONE', *, *, #32619, .F. ) ;
#6187=ORIENTED_EDGE ( 'NONE', *, *, #1987, .T. ) ;
#6228=CARTESIAN_POINT ( 'NONE',  ( -2.621328321948020346, -7.606199919102354379, -7.633618187056584681 ) ) ;
#6231=ORIENTED_EDGE ( 'NONE', *, *, #36604, .T. ) ;
#6403=VERTEX_POINT ( 'NONE', #24950 ) ;
#6445=CARTESIAN_POINT ( 'NONE',  ( 2.325424218458714165, -7.317669739337183898, -7.030005583191490715 ) ) ;
#6539=CARTESIAN_POINT ( 'NONE',  ( 7.922281120364393914, -4.573931137438282057, -8.047472243342932430 ) ) ;
#6605=ORIENTED_EDGE ( 'NONE', *, *, #9441, .T. ) ;
#6754=CARTESIAN_POINT ( 'NONE',  ( 0.9763930676190096802, -8.096533237419681228, -7.213065638943101376 ) ) ;
#6820=ORIENTED_EDGE ( 'NONE', *, *, #62648, .F. ) ;
#6856=AXIS2_PLACEMENT_3D ( 'NONE', #50299, #45472, #60284 ) ;
#6859=CARTESIAN_POINT ( 'NONE',  ( 7.914984360234579519, -3.818534719232097974, -7.907701344400643428 ) ) ;
#6876=EDGE_CURVE ( 'NONE', #4851, #38994, #17237, .T. ) ;
#6917=( BOUNDED_SURFACE ( )  B_SPLINE_SURFACE ( 3, 2, ( 
 ( #43893, #44861, #44218 ),
 ( #39707, #10773, #824 ),
 ( #59347, #53565, #9490 ),
 ( #63542, #19463, #59022 ),
 ( #14953, #59995, #60953 ),
 ( #31666, #31336, #16244 ),
 ( #51303, #55489, #60637 ),
 ( #21387, #56117, #26852 ) ),
 .UNSPECIFIED., .F., .F., .F. ) 
 B_SPLINE_SURFACE_WITH_KNOTS ( ( 4, 2, 2, 4 ),
 ( 3, 3 ),
 ( 0.03861844051980969222, 0.04325213341840641185, 0.04556897986770477166, 0.04788582631700313147 ),
 ( 0.000000000000000000, 1.000000000000000000 ),
 .UNSPECIFIED. ) 
 GEOMETRIC_REPRESENTATION_ITEM ( )  RATIONAL_B_SPLINE_SURFACE ( (
 ( 1.000000000000000000, 0.8047781759831921233, 1.000000000000000000),
 ( 1.000000000000000000, 0.8123762462806503049, 1.000000000000000000),
 ( 1.000000000000000000, 0.8190659850614813164, 1.000000000000000000),
 ( 1.000000000000000000, 0.8191937571014595854, 1.000000000000000000),
 ( 1.000000000000000000, 0.8176092952779865364, 1.000000000000000000),
 ( 1.000000000000000000, 0.8122962088597069918, 1.000000000000000000),
 ( 1.000000000000000000, 0.8086311330827506971, 1.000000000000000000),
 ( 1.000000000000000000, 0.8047712282214323221, 1.000000000000000000) ) ) 
 REPRESENTATION_ITEM ( '' )  SURFACE ( )  );
#6961=EDGE_LOOP ( 'NONE', ( #31831, #62520 ) ) ;
#7077=CARTESIAN_POINT ( 'NONE',  ( 4.419133455864432847, -6.108866147516184952, -7.026396753507086146 ) ) ;
#7088=B_SPLINE_CURVE_WITH_KNOTS ( 'NONE', 3,
 ( #24260, #13975, #53222, #14920, #39046, #34526 ),
 .UNSPECIFIED., .F., .F.,
 ( 4, 2, 4 ),
 ( -5.145455527296316946E-06, 0.0004153350442917489458, 0.0008358155441107941331 ),
 .UNSPECIFIED. ) ;
#7122=EDGE_LOOP ( 'NONE', ( #38425, #4575, #40285, #11179 ) ) ;
#7138=CARTESIAN_POINT ( 'NONE',  ( -1.250000000000000444, 7.938566201357357244, -7.198902722707429369 ) ) ;
#7173=CYLINDRICAL_SURFACE ( 'NONE', #14438, 5.000000000000000888 ) ;
#7274=CIRCLE ( 'NONE', #28774, 7.500000000000001776 ) ;
#7283=CARTESIAN_POINT ( 'NONE',  ( -7.500000000000000000, -2.571118828324945760, -0.3627527587569098766 ) ) ;
#7296=ORIENTED_EDGE ( 'NONE', *, *, #26443, .F. ) ;
#7521=DIRECTION ( 'NONE',  ( 1.000000000000000000, 0.000000000000000000, -0.000000000000000000 ) ) ;
#7598=CARTESIAN_POINT ( 'NONE',  ( -7.500000000000000000, -4.330127018922199866, -1.000000000000000888 ) ) ;
#7648=AXIS2_PLACEMENT_3D ( 'NONE', #10110, #15256, #40334 ) ;
#7739=CARTESIAN_POINT ( 'NONE',  ( -7.894787914004607998, -1.230850257101226302E-13, -7.591390474663425536 ) ) ;
#7788=CARTESIAN_POINT ( 'NONE',  ( 4.250000000000000000, 0.000000000000000000, -9.449444346342714240 ) ) ;
#7824=VECTOR ( 'NONE', #35713, 1000.000000000000000 ) ;
#7847=CARTESIAN_POINT ( 'NONE',  ( -5.000000000000000888, 6.123233995736767268E-16, -10.00000000000000000 ) ) ;
#7942=EDGE_CURVE ( 'NONE', #29821, #3756, #60198, .T. ) ;
#7964=VECTOR ( 'NONE', #29763, 1000.000000000000000 ) ;
#8014=ORIENTED_EDGE ( 'NONE', *, *, #26443, .T. ) ;
#8109=CARTESIAN_POINT ( 'NONE',  ( 5.040301471719072168, 5.750234626350511746, -0.09933465333851003443 ) ) ;
#8168=CARTESIAN_POINT ( 'NONE',  ( 0.000000000000000000, 0.000000000000000000, -9.974600000000000577 ) ) ;
#8235=EDGE_LOOP ( 'NONE', ( #8723, #3372, #29083, #6820, #20413, #58877, #47439 ) ) ;
#8398=CARTESIAN_POINT ( 'NONE',  ( 5.000000000000000888, 0.000000000000000000, -10.00000000000000000 ) ) ;
#8534=ORIENTED_EDGE ( 'NONE', *, *, #19984, .F. ) ;
#8591=UNCERTAINTY_MEASURE_WITH_UNIT (LENGTH_MEASURE( 1.000000000000000082E-05 ), #9273, 'distance_accuracy_value', 'NONE');
#8723=ORIENTED_EDGE ( 'NONE', *, *, #63433, .T. ) ;
#8906=CARTESIAN_POINT ( 'NONE',  ( -2.623433461001184686, 7.604994000793856124, -7.633824513837113912 ) ) ;
#8951=CIRCLE ( 'NONE', #44907, 10.39117206796836079 ) ;
#8964=DIRECTION ( 'NONE',  ( 1.000000000000000000, 0.000000000000000000, 0.000000000000000000 ) ) ;
#8992=FACE_OUTER_BOUND ( 'NONE', #46904, .T. ) ;
#9025=CARTESIAN_POINT ( 'NONE',  ( -7.897850199329715437, 1.533397866934075759, -7.634054012537968781 ) ) ;
#9205=CARTESIAN_POINT ( 'NONE',  ( -7.500000000000000000, 4.330127018922191873, -0.9999999999999970024 ) ) ;
#9273=( LENGTH_UNIT ( ) NAMED_UNIT ( * ) SI_UNIT ( .MILLI., .METRE. ) );
#9367=LINE ( 'NONE', #19652, #56537 ) ;
#9399=EDGE_CURVE ( 'NONE', #38994, #13010, #28775, .T. ) ;
#9441=EDGE_CURVE ( 'NONE', #48710, #49422, #43425, .T. ) ;
#9490=CARTESIAN_POINT ( 'NONE',  ( 5.335963852943280017, 6.035591050531201596, -7.593821156097048330 ) ) ;
#9531=CARTESIAN_POINT ( 'NONE',  ( -6.601567268551443490, 5.319966374295965750, -7.792327460285856766 ) ) ;
#9536=EDGE_CURVE ( 'NONE', #29985, #3756, #14262, .T. ) ;
#9573=CARTESIAN_POINT ( 'NONE',  ( -7.915341292092594294, -3.857523022641989652, -7.913710289178173873 ) ) ;
#9577=B_SPLINE_CURVE_WITH_KNOTS ( 'NONE', 3,
 ( #27460, #27776, #61576, #61895, #37438, #17511 ),
 .UNSPECIFIED., .F., .F.,
 ( 4, 2, 4 ),
 ( 2.475503369212747145E-07, 0.002222330217055634109, 0.004444412883774346255 ),
 .UNSPECIFIED. ) ;
#9678=AXIS2_PLACEMENT_3D ( 'NONE', #4259, #14209, #59566 ) ;
#9691=B_SPLINE_CURVE_WITH_KNOTS ( 'NONE', 3,
 ( #9205, #201, #23698, #4076, #19481, #43296 ),
 .UNSPECIFIED., .F., .F.,
 ( 4, 2, 4 ),
 ( 2.475503369207376426E-07, 0.002222330217055627170, 0.004444412883774334112 ),
 .UNSPECIFIED. ) ;
#9828=CARTESIAN_POINT ( 'NONE',  ( -4.250000000000000000, 5.204748896376250699E-16, -0.5251556536572846712 ) ) ;
#9834=CARTESIAN_POINT ( 'NONE',  ( -4.599534470795546781, 6.460478697738500031, -7.590212325761530821 ) ) ;
#9873=SHAPE_DEFINITION_REPRESENTATION ( #43520, #14320 ) ;
#9898=CARTESIAN_POINT ( 'NONE',  ( -0.6508621380849236582, -8.763657152406455708, -7.907633014911225722 ) ) ;
#9964=EDGE_CURVE ( 'NONE', #6403, #57220, #30571, .T. ) ;
#9965=DIRECTION ( 'NONE',  ( 0.000000000000000000, 0.000000000000000000, 1.000000000000000000 ) ) ;
#9985=CARTESIAN_POINT ( 'NONE',  ( -7.703920929261744099, 4.447860822324859242, -7.917989418073275942 ) ) ;
#10017=DIRECTION ( 'NONE',  ( 1.000000000000000000, 0.000000000000000000, 0.000000000000000000 ) ) ;
#10077=CARTESIAN_POINT ( 'NONE',  ( -5.007715329123872641E-16, -8.660254037844399733, -7.422398894150038728 ) ) ;
#10093=CONICAL_SURFACE ( 'NONE', #3909, 10.39117206796836079, 1.221730476396047926 ) ;
#10110=CARTESIAN_POINT ( 'NONE',  ( 0.000000000000000000, 0.000000000000000000, -0.5776712190230133270 ) ) ;
#10180=ORIENTED_EDGE ( 'NONE', *, *, #47925, .T. ) ;
#10199=ORIENTED_EDGE ( 'NONE', *, *, #22100, .T. ) ;
#10291=EDGE_LOOP ( 'NONE', ( #45407, #36195, #16851, #4288 ) ) ;
#10314=AXIS2_PLACEMENT_3D ( 'NONE', #61842, #43139, #3299 ) ;
#10444=CARTESIAN_POINT ( 'NONE',  ( 7.500000000000000000, -3.608439182435168036, -7.298562697733107285 ) ) ;
#10536=CARTESIAN_POINT ( 'NONE',  ( -3.280815508853482498, -7.221948645665452915, -7.591546097228404122 ) ) ;
#10654=ORIENTED_EDGE ( 'NONE', *, *, #38067, .T. ) ;
#10682=ADVANCED_FACE ( 'NONE', ( #56815 ), #10093, .T. ) ;
#10769=CARTESIAN_POINT ( 'NONE',  ( 7.500000000000000000, 2.886751345948125547, -7.198902722707427593 ) ) ;
#10773=CARTESIAN_POINT ( 'NONE',  ( 6.484173630542770184, 4.916614646782027087, -7.642786413619098163 ) ) ;
#10843=CARTESIAN_POINT ( 'NONE',  ( -7.500000000000000000, -3.948305025207388130, -7.349903712356284480 ) ) ;
#11125=CARTESIAN_POINT ( 'NONE',  ( -6.902527771671634227, -4.675077770780906583, -0.7026937717022867513 ) ) ;
#11179=ORIENTED_EDGE ( 'NONE', *, *, #3236, .F. ) ;
#11250=FACE_OUTER_BOUND ( 'NONE', #7122, .T. ) ;
#11284=( GEOMETRIC_REPRESENTATION_CONTEXT ( 3 ) GLOBAL_UNCERTAINTY_ASSIGNED_CONTEXT ( ( #33926 ) ) GLOBAL_UNIT_ASSIGNED_CONTEXT ( ( #27925, #13141, #57845 ) ) REPRESENTATION_CONTEXT ( 'NONE', 'WORKASPACE' ) );
#11364=CARTESIAN_POINT ( 'NONE',  ( 7.499999999999999112, 0.7577384720672989404, -7.446470314338469620 ) ) ;
#11383=FACE_OUTER_BOUND ( 'NONE', #19629, .T. ) ;
#11590=DIRECTION ( 'NONE',  ( -1.000000000000000000, 0.000000000000000000, 0.000000000000000000 ) ) ;
#11623=ORIENTED_EDGE ( 'NONE', *, *, #36274, .F. ) ;
#11666=CARTESIAN_POINT ( 'NONE',  ( -1.282512619719133662, -8.391164935524759727, -7.795653906409117262 ) ) ;
#11725=CARTESIAN_POINT ( 'NONE',  ( 7.500000000000000888, -0.7512838658081439913, 1.423015351387224570E-15 ) ) ;
#11751=EDGE_CURVE ( 'NONE', #35203, #53762, #15955, .T. ) ;
#11939=CIRCLE ( 'NONE', #32512, 0.7733184030943203169 ) ;
#12000=CARTESIAN_POINT ( 'NONE',  ( 7.908217798048221781, 3.084840533507044125, -7.795645399445156443 ) ) ;
#12009=DIRECTION ( 'NONE',  ( 0.000000000000000000, 0.000000000000000000, 1.000000000000000000 ) ) ;
#12026=CARTESIAN_POINT ( 'NONE',  ( 4.606548227981508425, 6.456511556909250160, -7.591235721156633254 ) ) ;
#12087=CARTESIAN_POINT ( 'NONE',  ( -7.500000000000000000, -3.988190556646204588, -0.8526458641284329065 ) ) ;
#12177=EDGE_LOOP ( 'NONE', ( #31316, #49850, #8534, #19262 ) ) ;
#12179=B_SPLINE_CURVE_WITH_KNOTS ( 'NONE', 3,
 ( #45509, #1472, #60324, #16250, #20110, #50658, #11725, #1794 ),
 .UNSPECIFIED., .F., .F.,
 ( 4, 2, 2, 4 ),
 ( 0.006061689441712453386, 0.007174127271521678166, 0.008286565101330902947, 0.01051144076094935251 ),
 .UNSPECIFIED. ) ;
#12210=CARTESIAN_POINT ( 'NONE',  ( -10.12668159690567649, 1.256356190803088863E-15, -9.999999999999998224 ) ) ;
#12259=DIRECTION ( 'NONE',  ( -1.000000000000000000, 0.000000000000000000, 0.000000000000000000 ) ) ;
#12274=CARTESIAN_POINT ( 'NONE',  ( -2.500000000000000000, 7.216878364870324525, -7.063244554130001518 ) ) ;
#12325=ORIENTED_EDGE ( 'NONE', *, *, #59513, .T. ) ;
#12332=CARTESIAN_POINT ( 'NONE',  ( 7.908230272950877549, -3.123266379887881250, -7.776722524729575703 ) ) ;
#12356=VECTOR ( 'NONE', #2047, 1000.000000000000114 ) ;
#12522=CARTESIAN_POINT ( 'NONE',  ( 7.549006887134058985, 4.358421158401185380, -7.700127545397291939 ) ) ;
#12523=CARTESIAN_POINT ( 'NONE',  ( 2.352174619736673744, -7.302225387959338399, -7.450218641350605076 ) ) ;
#12658=EDGE_LOOP ( 'NONE', ( #36090, #24682, #30429, #52474 ) ) ;
#12723=CARTESIAN_POINT ( 'NONE',  ( 0.000000000000000000, 0.000000000000000000, 0.000000000000000000 ) ) ;
#12771=CIRCLE ( 'NONE', #9678, 5.000000000000001776 ) ;
#12915=ADVANCED_FACE ( 'NONE', ( #60287, #17490 ), #3019, .T. ) ;
#12931=EDGE_CURVE ( 'NONE', #13010, #23656, #25054, .T. ) ;
#12977=CARTESIAN_POINT ( 'NONE',  ( -6.127431526422343306E-17, 9.147862274876549904, -8.047472243342932430 ) ) ;
#13001=CARTESIAN_POINT ( 'NONE',  ( -2.459698528280933161, 7.240146430416066536, -0.09933465333851029810 ) ) ;
#13010=VERTEX_POINT ( 'NONE', #28073 ) ;
#13031=CARTESIAN_POINT ( 'NONE',  ( -5.000000000000001776, 0.000000000000000000, -9.974600000000000577 ) ) ;
#13084=AXIS2_PLACEMENT_3D ( 'NONE', #47784, #29407, #52622 ) ;
#13126=EDGE_LOOP ( 'NONE', ( #17933, #50162, #44198, #16350 ) ) ;
#13140=ORIENTED_EDGE ( 'NONE', *, *, #15362, .T. ) ;
#13141=( NAMED_UNIT ( * ) PLANE_ANGLE_UNIT ( ) SI_UNIT ( $, .RADIAN. ) );
#13203=ORIENTED_EDGE ( 'NONE', *, *, #44444, .T. ) ;
#13323=DIRECTION ( 'NONE',  ( 1.000000000000000000, 0.000000000000000000, 0.000000000000000000 ) ) ;
#13460=SURFACE_SIDE_STYLE ('',( #62357 ) ) ;
#13562=CARTESIAN_POINT ( 'NONE',  ( 7.500000000000000000, 4.330127018922199866, -1.000000000000000888 ) ) ;
#13610=ORIENTED_EDGE ( 'NONE', *, *, #28689, .F. ) ;
#13700=CARTESIAN_POINT ( 'NONE',  ( -7.499999999999998224, -4.330127018922197202, -7.564335161054478895 ) ) ;
#13730=CARTESIAN_POINT ( 'NONE',  ( -7.264118654998712010, 4.945491722146218905, -7.907633014911216840 ) ) ;
#13733=AXIS2_PLACEMENT_3D ( 'NONE', #47860, #27622, #3819 ) ;
#13735=DIRECTION ( 'NONE',  ( 1.000000000000000000, 0.000000000000000000, 0.000000000000000000 ) ) ;
#13763=PRESENTATION_STYLE_ASSIGNMENT (( #23110 ) ) ;
#13792=B_SPLINE_CURVE_WITH_KNOTS ( 'NONE', 3,
 ( #36396, #27372, #7138, #12274, #26753, #31888, #42168, #61175, #61804 ),
 .UNSPECIFIED., .F., .F.,
 ( 4, 2, 1, 2, 4 ),
 ( 0.000000000000000000, 0.002165063509461098365, 0.004330127018922195863, 0.006495190528383293360, 0.008660254037844389990 ),
 .UNSPECIFIED. ) ;
#13827=CARTESIAN_POINT ( 'NONE',  ( 7.500000000000001776, 0.000000000000000000, 0.000000000000000000 ) ) ;
#13845=CARTESIAN_POINT ( 'NONE',  ( -7.894787914004607998, -1.230850257101226302E-13, -7.591390474663425536 ) ) ;
#13897=CARTESIAN_POINT ( 'NONE',  ( 0.000000000000000000, 0.000000000000000000, 0.000000000000000000 ) ) ;
#13914=EDGE_LOOP ( 'NONE', ( #10654, #47424, #58850, #7296 ) ) ;
#13919=DIRECTION ( 'NONE',  ( 1.000000000000000000, 0.000000000000000000, 0.000000000000000000 ) ) ;
#13975=CARTESIAN_POINT ( 'NONE',  ( -2.249002180491467900E-14, 9.016154170237591359, -7.999534413642735764 ) ) ;
#14179=VERTEX_POINT ( 'NONE', #62588 ) ;
#14209=DIRECTION ( 'NONE',  ( -0.000000000000000000, -0.000000000000000000, 1.000000000000000000 ) ) ;
#14262=B_SPLINE_CURVE_WITH_KNOTS ( 'NONE', 3,
 ( #26790, #1729, #17769, #46721, #6859, #6539 ),
 .UNSPECIFIED., .F., .F.,
 ( 4, 2, 4 ),
 ( 0.004615310220740742597, 0.006918661718823353700, 0.009222013216905964803 ),
 .UNSPECIFIED. ) ;
#14306=FACE_OUTER_BOUND ( 'NONE', #48091, .T. ) ;
#14320=SHAPE_REPRESENTATION ( 'hex flange nut gradea_iso_ISO - 4161 - M10 - N', ( #43054 ), #24596 ) ;
#14355=CARTESIAN_POINT ( 'NONE',  ( 0.04606493828584144051, 9.175055303659556571, -8.057411785091790790 ) ) ;
#14396=CARTESIAN_POINT ( 'NONE',  ( -7.908228835406498902, 3.123118350879302341, -7.776694659841278501 ) ) ;
#14438=AXIS2_PLACEMENT_3D ( 'NONE', #46400, #21645, #56699 ) ;
#14448=ORIENTED_EDGE ( 'NONE', *, *, #19984, .T. ) ;
#14485=CARTESIAN_POINT ( 'NONE',  ( 0.000000000000000000, 0.000000000000000000, 0.000000000000000000 ) ) ;
#14518=DIRECTION ( 'NONE',  ( 1.000000000000000000, 0.000000000000000000, 0.000000000000000000 ) ) ;
#14577=EDGE_CURVE ( 'NONE', #37707, #26290, #22517, .T. ) ;
#14630=FACE_OUTER_BOUND ( 'NONE', #12658, .T. ) ;
#14709=CARTESIAN_POINT ( 'NONE',  ( -7.500000000000346390, -3.105855721450154316, -7.659356991636309786 ) ) ;
#14713=ORIENTED_EDGE ( 'NONE', *, *, #47658, .F. ) ;
#14787=ORIENTED_EDGE ( 'NONE', *, *, #42120, .F. ) ;
#14807=CARTESIAN_POINT ( 'NONE',  ( 6.874999999999997335, -4.690970937165716670, -7.298562697733105509 ) ) ;
#14833=CARTESIAN_POINT ( 'NONE',  ( 0.000000000000000000, 0.000000000000000000, -0.5251556536572846712 ) ) ;
#14902=CARTESIAN_POINT ( 'NONE',  ( 7.894787914004607998, 1.243647571710251278E-13, -7.591390474663425536 ) ) ;
#14920=CARTESIAN_POINT ( 'NONE',  ( -5.134616530693496727E-16, 8.716839668575667943, -7.700121441565823233 ) ) ;
#14953=CARTESIAN_POINT ( 'NONE',  ( 2.387978478801324300, 7.281554020289410012, -7.069802615102035226 ) ) ;
#14988=CARTESIAN_POINT ( 'NONE',  ( -6.486836893983275232, 4.915077010913945443, -7.231838333420560261 ) ) ;
#14989=CARTESIAN_POINT ( 'NONE',  ( -6.127431526422343306E-17, 9.147862274876549904, -8.047472243342932430 ) ) ;
#15048=DIRECTION ( 'NONE',  ( 1.000000000000000000, 0.000000000000000000, 0.000000000000000000 ) ) ;
#15130=LINE ( 'NONE', #49853, #7824 ) ;
#15223=CARTESIAN_POINT ( 'NONE',  ( 3.096526599377912525, -6.872473572140722631, -5.976664475826341615E-15 ) ) ;
#15256=DIRECTION ( 'NONE',  ( -0.000000000000000000, -0.000000000000000000, 1.000000000000000000 ) ) ;
#15362=EDGE_CURVE ( 'NONE', #22221, #4851, #13792, .T. ) ;
#15555=CARTESIAN_POINT ( 'NONE',  ( -3.749999999999998224, -6.495190528383296247, -6.991905250253752868 ) ) ;
#15601=CARTESIAN_POINT ( 'NONE',  ( 7.500000000000000000, -5.637851296924623057E-15, -6.991905250253753756 ) ) ;
#15643=FACE_OUTER_BOUND ( 'NONE', #23072, .T. ) ;
#15677=CARTESIAN_POINT ( 'NONE',  ( -7.499999999999999112, 4.651022038490018495, -7.928862870699868282 ) ) ;
#15732=VERTEX_POINT ( 'NONE', #35058 ) ;
#15756=DIRECTION ( 'NONE',  ( 1.000000000000000000, 0.000000000000000000, 0.000000000000000000 ) ) ;
#15759=VECTOR ( 'NONE', #58471, 1000.000000000000000 ) ;
#15780=EDGE_CURVE ( 'NONE', #49422, #50022, #37537, .T. ) ;
#15838=CARTESIAN_POINT ( 'NONE',  ( 0.000000000000000000, 0.000000000000000000, -8.499999999999998224 ) ) ;
#15860=DIRECTION ( 'NONE',  ( 1.000000000000000000, 0.000000000000000000, 0.000000000000000000 ) ) ;
#15870=CARTESIAN_POINT ( 'NONE',  ( 3.750000000000004441, -6.495190528383289141, 0.000000000000000000 ) ) ;
#15886=CARTESIAN_POINT ( 'NONE',  ( 7.922811941611899833, 4.628808333142401032, -8.057670691780701944 ) ) ;
#15916=CARTESIAN_POINT ( 'NONE',  ( 7.500000000000000000, -4.330127018922199866, -7.422398894150035176 ) ) ;
#15955=B_SPLINE_CURVE_WITH_KNOTS ( 'NONE', 3,
 ( #42999, #13730, #9531, #5026, #28522, #24645, #8906, #4091, #62644, #14989 ),
 .UNSPECIFIED., .F., .F.,
 ( 4, 2, 2, 2, 4 ),
 ( 0.000000000000000000, 0.002305503304226491634, 0.004611006608452983269, 0.006916509912679474036, 0.009222013216905963068 ),
 .UNSPECIFIED. ) ;
#16006=CARTESIAN_POINT ( 'NONE',  ( -7.640563834021360018E-16, -9.147862274876560562, -8.047472243342937759 ) ) ;
#16244=CARTESIAN_POINT ( 'NONE',  ( 1.282512619718868541, 8.391164935524033197, -7.795653906408837486 ) ) ;
#16250=CARTESIAN_POINT ( 'NONE',  ( 7.499999999999999112, -2.930060224340428565, -0.4701183149080248036 ) ) ;
#16277=CARTESIAN_POINT ( 'NONE',  ( -7.970070017554212960, 4.546953124339755625, -8.057670357645356773 ) ) ;
#16350=ORIENTED_EDGE ( 'NONE', *, *, #59851, .F. ) ;
#16471=DIRECTION ( 'NONE',  ( 1.000000000000000000, 0.000000000000000000, 0.000000000000000000 ) ) ;
#16721=CARTESIAN_POINT ( 'NONE',  ( 6.439685834477092641, -4.942299687812566233, -7.659344964963564983 ) ) ;
#16820=CARTESIAN_POINT ( 'NONE',  ( -3.080866544137490504, -6.881514909249304424, -7.026396753507435200 ) ) ;
#16833=CARTESIAN_POINT ( 'NONE',  ( 7.500000000000000000, 1.572594658376109011, -7.069792055233639516 ) ) ;
#16841=CARTESIAN_POINT ( 'NONE',  ( -7.640563834021360018E-16, -9.147862274876560562, -8.047472243342937759 ) ) ;
#16851=ORIENTED_EDGE ( 'NONE', *, *, #12931, .F. ) ;
#16961=( BOUNDED_SURFACE ( )  B_SPLINE_SURFACE ( 3, 2, ( 
 ( #33977, #49723, #14355 ),
 ( #59062, #24644, #53598 ),
 ( #530, #5025, #19495 ),
 ( #39110, #58738, #9834 ),
 ( #49078, #44251, #215 ),
 ( #14988, #34598, #60030 ),
 ( #41339, #55835, #25918 ),
 ( #51008, #45536, #16277 ) ),
 .UNSPECIFIED., .F., .F., .F. ) 
 B_SPLINE_SURFACE_WITH_KNOTS ( ( 4, 2, 2, 4 ),
 ( 3, 3 ),
 ( 0.03861844051980969916, 0.04325213341840641879, 0.04556897986770477860, 0.04788582631700313841 ),
 ( 0.000000000000000000, 1.000000000000000000 ),
 .UNSPECIFIED. ) 
 GEOMETRIC_REPRESENTATION_ITEM ( )  RATIONAL_B_SPLINE_SURFACE ( (
 ( 1.000000000000000000, 0.8047781759831920123, 1.000000000000000000),
 ( 1.000000000000000000, 0.8123762462803147955, 1.000000000000000000),
 ( 1.000000000000000000, 0.8190659850619289584, 1.000000000000000000),
 ( 1.000000000000000000, 0.8191937571012362085, 1.000000000000000000),
 ( 1.000000000000000000, 0.8176092952779873135, 1.000000000000000000),
 ( 1.000000000000000000, 0.8122962088597077690, 1.000000000000000000),
 ( 1.000000000000000000, 0.8086311330827508081, 1.000000000000000000),
 ( 1.000000000000000000, 0.8047712282214326551, 1.000000000000000000) ) ) 
 REPRESENTATION_ITEM ( '' )  SURFACE ( )  );
#17134=AXIS2_PLACEMENT_3D ( 'NONE', #34709, #44347, #48859 ) ;
#17143=ORIENTED_EDGE ( 'NONE', *, *, #14577, .F. ) ;
#17179=ORIENTED_EDGE ( 'NONE', *, *, #35730, .F. ) ;
#17237=B_SPLINE_CURVE_WITH_KNOTS ( 'NONE', 3,
 ( #36986, #22193, #20359, #55414, #44787, #41794, #59605, #749, #61438 ),
 .UNSPECIFIED., .F., .F.,
 ( 4, 2, 1, 2, 4 ),
 ( 0.000000000000000000, 0.002165063509461097498, 0.004330127018922194995, 0.006495190528383292493, 0.008660254037844389990 ),
 .UNSPECIFIED. ) ;
#17290=FACE_OUTER_BOUND ( 'NONE', #30285, .T. ) ;
#17402=ADVANCED_FACE ( 'NONE', ( #451 ), #20055, .F. ) ;
#17490=FACE_OUTER_BOUND ( 'NONE', #57182, .T. ) ;
#17511=CARTESIAN_POINT ( 'NONE',  ( 3.750000000000005329, 6.495190528383288253, 0.000000000000000000 ) ) ;
#17762=CARTESIAN_POINT ( 'NONE',  ( -5.000000000000001776, 0.000000000000000000, -9.974600000000000577 ) ) ;
#17769=CARTESIAN_POINT ( 'NONE',  ( 7.897850199329715437, -1.533397866934079312, -7.634054012537967893 ) ) ;
#17829=CARTESIAN_POINT ( 'NONE',  ( 4.336808689942017736E-16, 8.660254037844390851, -1.000000000000000888 ) ) ;
#17870=AXIS2_PLACEMENT_3D ( 'NONE', #20523, #63631, #15048 ) ;
#17871=ADVANCED_FACE ( 'NONE', ( #5910 ), #57696, .F. ) ;
#17933=ORIENTED_EDGE ( 'NONE', *, *, #5989, .F. ) ;
#17998=CONICAL_SURFACE ( 'NONE', #21086, 4.174999999999999822, 0.9599310885968795892 ) ;
#18023=DIRECTION ( 'NONE',  ( 0.000000000000000000, 0.000000000000000000, -1.000000000000000000 ) ) ;
#18068=CARTESIAN_POINT ( 'NONE',  ( 5.000000000000000888, 0.000000000000000000, -25.03750572909317285 ) ) ;
#18118=CARTESIAN_POINT ( 'NONE',  ( 0.000000000000000000, 0.000000000000000000, -9.449444346342714240 ) ) ;
#18120=CARTESIAN_POINT ( 'NONE',  ( 1.306442393143578906, 8.377108146505383601, -7.792327460285857654 ) ) ;
#18399=DIRECTION ( 'NONE',  ( 0.000000000000000000, 0.000000000000000000, 1.000000000000000000 ) ) ;
#18687=CARTESIAN_POINT ( 'NONE',  ( 7.922281120364393914, -4.573931137438282057, -8.047472243342932430 ) ) ;
#18695=CARTESIAN_POINT ( 'NONE',  ( 1.249999999999999112, -7.938566201357367902, -7.198902722707431145 ) ) ;
#18800=EDGE_CURVE ( 'NONE', #63519, #41293, #27726, .T. ) ;
#18816=CIRCLE ( 'NONE', #53758, 7.500000000000001776 ) ;
#18831=CARTESIAN_POINT ( 'NONE',  ( 0.000000000000000000, 0.000000000000000000, 0.000000000000000000 ) ) ;
#18894=ORIENTED_EDGE ( 'NONE', *, *, #32619, .T. ) ;
#18910=CIRCLE ( 'NONE', #17870, 5.000000000000000888 ) ;
#18994=CARTESIAN_POINT ( 'NONE',  ( 6.601567268551444378, -5.319966374295973743, -7.792327460285856766 ) ) ;
#19088=CARTESIAN_POINT ( 'NONE',  ( 7.499999999999999112, -4.330127018922205195, -1.000000000000000888 ) ) ;
#19106=CARTESIAN_POINT ( 'NONE',  ( 7.499999999999999112, -4.330127018922205195, -1.000000000000000888 ) ) ;
#19157=CARTESIAN_POINT ( 'NONE',  ( -7.907996613752304782, -3.055722423191990611, -7.792112796859422374 ) ) ;
#19218=CARTESIAN_POINT ( 'NONE',  ( -5.007715329123872641E-16, -8.660254037844399733, -10.00000000000000000 ) ) ;
#19235=ORIENTED_EDGE ( 'NONE', *, *, #35914, .F. ) ;
#19262=ORIENTED_EDGE ( 'NONE', *, *, #62480, .F. ) ;
#19369=B_SPLINE_CURVE_WITH_KNOTS ( 'NONE', 3,
 ( #16006, #9898, #39800, #39167, #10536, #19553, #44960, #58792, #34997, #29507 ),
 .UNSPECIFIED., .F., .F.,
 ( 4, 2, 2, 2, 4 ),
 ( 0.000000000000000000, 0.002305503304226489900, 0.004611006608452982401, 0.006916509912679474036, 0.009222013216905966537 ),
 .UNSPECIFIED. ) ;
#19419=CARTESIAN_POINT ( 'NONE',  ( 7.500000000000000000, 4.330127018922190096, -10.00000000000000000 ) ) ;
#19463=CARTESIAN_POINT ( 'NONE',  ( 3.093533885183100018, 6.874201416487501604, -7.446478553995813598 ) ) ;
#19469=PLANE ( 'NONE',  #41934 ) ;
#19477=B_SPLINE_CURVE_WITH_KNOTS ( 'NONE', 3,
 ( #47646, #27087, #8109, #36742, #2340, #13562 ),
 .UNSPECIFIED., .F., .F.,
 ( 4, 2, 4 ),
 ( 0.004444412883774346255, 0.006655097293744437204, 0.008865781703714529019 ),
 .UNSPECIFIED. ) ;
#19481=CARTESIAN_POINT ( 'NONE',  ( -4.406842699996122548, 6.115962218725288224, 1.165517335421917267E-15 ) ) ;
#19495=CARTESIAN_POINT ( 'NONE',  ( -2.558993250147282073, 7.638875775587784744, -7.593821156097241065 ) ) ;
#19553=CARTESIAN_POINT ( 'NONE',  ( -4.606548227981510202, -6.456511556909259930, -7.591235721156638583 ) ) ;
#19557=( NAMED_UNIT ( * ) SI_UNIT ( $, .STERADIAN. ) SOLID_ANGLE_UNIT ( ) );
#19620=ADVANCED_FACE ( 'NONE', ( #36453 ), #45701, .F. ) ;
#19629=EDGE_LOOP ( 'NONE', ( #14448, #23109, #40407, #34517 ) ) ;
#19652=CARTESIAN_POINT ( 'NONE',  ( -4.174999999999999822, 5.112900386440199535E-16, -0.5776712190230133270 ) ) ;
#19672=DIRECTION ( 'NONE',  ( 1.000000000000000000, 0.000000000000000000, 0.000000000000000000 ) ) ;
#19824=VERTEX_POINT ( 'NONE', #58906 ) ;
#19825=CARTESIAN_POINT ( 'NONE',  ( -7.500000000000000000, 4.330127018922191873, -7.422398894150032511 ) ) ;
#19930=PRODUCT ( 'hex flange nut gradea_iso_ISO - 4161 - M10 - N', 'hex flange nut gradea_iso_ISO - 4161 - M10 - N', '', ( #249 ) ) ;
#19975=EDGE_CURVE ( 'NONE', #31318, #4973, #22606, .T. ) ;
#19984=EDGE_CURVE ( 'NONE', #32825, #29058, #3096, .T. ) ;
#20033=B_SPLINE_CURVE_WITH_KNOTS ( 'NONE', 3,
 ( #44703, #668, #5798, #45990, #1322, #39878, #50176, #41153, #50507 ),
 .UNSPECIFIED., .F., .F.,
 ( 4, 2, 1, 2, 4 ),
 ( 0.000000000000000000, 0.002165063509461097498, 0.004330127018922194995, 0.006495190528383292493, 0.008660254037844389990 ),
 .UNSPECIFIED. ) ;
#20050=CARTESIAN_POINT ( 'NONE',  ( 2.459698528280935825, -7.240146430416073642, -0.09933465333851955459 ) ) ;
#20055=PLANE ( 'NONE',  #3048 ) ;
#20110=CARTESIAN_POINT ( 'NONE',  ( 7.500000000000000000, -2.571118828324946648, -0.3627527587569098766 ) ) ;
#20185=CARTESIAN_POINT ( 'NONE',  ( -7.500000000000000000, -3.882691789160215290, -7.781695678273567118 ) ) ;
#20206=CONICAL_SURFACE ( 'NONE', #31488, 7.500000000000001776, 0.8594454914424796144 ) ;
#20340=CARTESIAN_POINT ( 'NONE',  ( -7.922281120364393914, 4.573931137438271399, -8.047472243342930653 ) ) ;
#20359=CARTESIAN_POINT ( 'NONE',  ( -7.500000000000000888, 2.886751345948126435, -7.198902722707427593 ) ) ;
#20413=ORIENTED_EDGE ( 'NONE', *, *, #35730, .T. ) ;
#20512=CARTESIAN_POINT ( 'NONE',  ( -7.500000000000000000, -4.732323933430407692, -7.493854309896101462 ) ) ;
#20523=CARTESIAN_POINT ( 'NONE',  ( 0.000000000000000000, 0.000000000000000000, -10.00000000000000000 ) ) ;
#20629=DIRECTION ( 'NONE',  ( -0.000000000000000000, -0.000000000000000000, 1.000000000000000000 ) ) ;
#20704=CARTESIAN_POINT ( 'NONE',  ( -5.000000000000000000, -5.773502691896264416, -7.063244554130003294 ) ) ;
#20708=CARTESIAN_POINT ( 'NONE',  ( -5.147825380260782957, -5.688155668810408017, -7.450218641351304960 ) ) ;
#20737=DIRECTION ( 'NONE',  ( 0.000000000000000000, 0.000000000000000000, 1.000000000000000000 ) ) ;
#20854=EDGE_CURVE ( 'NONE', #32825, #26290, #61211, .T. ) ;
#20933=EDGE_CURVE ( 'NONE', #28539, #21365, #27772, .T. ) ;
#21052=VERTEX_POINT ( 'NONE', #54 ) ;
#21086=AXIS2_PLACEMENT_3D ( 'NONE', #34544, #44524, #4652 ) ;
#21125=EDGE_CURVE ( 'NONE', #29058, #37707, #9367, .T. ) ;
#21206=EDGE_CURVE ( 'NONE', #4973, #14179, #7274, .T. ) ;
#21228=CARTESIAN_POINT ( 'NONE',  ( 6.625705691649528717, -5.306270977113132226, -7.795653906408932521 ) ) ;
#21258=CARTESIAN_POINT ( 'NONE',  ( 0.000000000000000000, 0.000000000000000000, -8.499999999999998224 ) ) ;
#21365=VERTEX_POINT ( 'NONE', #49872 ) ;
#21387=CARTESIAN_POINT ( 'NONE',  ( -0.3483149870578547969, 8.861353789385022495, -7.493854785173811983 ) ) ;
#21415=DIRECTION ( 'NONE',  ( 1.000000000000000000, 0.000000000000000000, 0.000000000000000000 ) ) ;
#21645=DIRECTION ( 'NONE',  ( -0.000000000000000000, -0.000000000000000000, 1.000000000000000000 ) ) ;
#21673=CARTESIAN_POINT ( 'NONE',  ( 7.500000000000000000, -3.202733125947433201, -7.213074474936314928 ) ) ;
#21708=CARTESIAN_POINT ( 'NONE',  ( 7.500000000000000000, 4.330127018922190096, -7.422398894150032511 ) ) ;
#21731=ADVANCED_FACE ( 'NONE', ( #30093 ), #16961, .F. ) ;
#21851=DIRECTION ( 'NONE',  ( -0.8660254037844382635, 0.5000000000000005551, 0.000000000000000000 ) ) ;
#21865=CARTESIAN_POINT ( 'NONE',  ( -7.500000000000000000, 4.330127018922191873, -0.9999999999999970024 ) ) ;
#21868=CARTESIAN_POINT ( 'NONE',  ( -10.39117206796836257, 1.272551561242683764E-15, -8.499999999999998224 ) ) ;
#21983=CARTESIAN_POINT ( 'NONE',  ( 7.922798488042200660, -4.627419312545550056, -8.057411459260041653 ) ) ;
#22008=CARTESIAN_POINT ( 'NONE',  ( 6.602753909532903087, 5.319290460493537154, -7.792447862505332168 ) ) ;
#22078=VERTEX_POINT ( 'NONE', #26884 ) ;
#22100=EDGE_CURVE ( 'NONE', #19824, #28539, #32969, .T. ) ;
#22185=CARTESIAN_POINT ( 'NONE',  ( 6.486836893983020325, -4.915077010914103539, -7.231838333420563814 ) ) ;
#22193=CARTESIAN_POINT ( 'NONE',  ( -7.500000000000000000, 3.608439182435158710, -7.298562697733104621 ) ) ;
#22221=VERTEX_POINT ( 'NONE', #54151 ) ;
#22286=DIRECTION ( 'NONE',  ( -0.000000000000000000, -0.000000000000000000, 1.000000000000000000 ) ) ;
#22337=B_SPLINE_CURVE_WITH_KNOTS ( 'NONE', 3,
 ( #18687, #54041, #18994, #29267, #59200, #3907, #34103, #29591, #63084, #43751 ),
 .UNSPECIFIED., .F., .F.,
 ( 4, 2, 2, 2, 4 ),
 ( 0.000000000000000000, 0.002305503304226490767, 0.004611006608452981534, 0.006916509912679473168, 0.009222013216905964803 ),
 .UNSPECIFIED. ) ;
#22475=B_SPLINE_CURVE_WITH_KNOTS ( 'NONE', 3,
 ( #24789, #5171, #18695, #44395, #40, #43759, #58876, #14807, #34112 ),
 .UNSPECIFIED., .F., .F.,
 ( 4, 2, 1, 2, 4 ),
 ( 6.245710625686469831E-20, 0.002165063509461098365, 0.004330127018922195863, 0.006495190528383293360, 0.008660254037844389990 ),
 .UNSPECIFIED. ) ;
#22502=CARTESIAN_POINT ( 'NONE',  ( -7.500000000000000000, 1.854554393013821745, -0.1880126015361722192 ) ) ;
#22505=CARTESIAN_POINT ( 'NONE',  ( 7.922281120364393914, 4.573931137438269623, -8.047472243342930653 ) ) ;
#22508=VECTOR ( 'NONE', #34451, 1000.000000000000000 ) ;
#22517=CIRCLE ( 'NONE', #32789, 5.000000000000000888 ) ;
#22606=CIRCLE ( 'NONE', #30808, 7.500000000000001776 ) ;
#22707=ORIENTED_EDGE ( 'NONE', *, *, #25848, .T. ) ;
#22734=DIRECTION ( 'NONE',  ( 1.000000000000000000, 0.000000000000000000, 0.000000000000000000 ) ) ;
#22775=CARTESIAN_POINT ( 'NONE',  ( 0.000000000000000000, 0.000000000000000000, -10.00000000000000000 ) ) ;
#22886=CARTESIAN_POINT ( 'NONE',  ( -7.908030677224553884, 3.059924800338342799, -7.792662696733364314 ) ) ;
#23072=EDGE_LOOP ( 'NONE', ( #2739, #6018, #40224, #2157 ) ) ;
#23109=ORIENTED_EDGE ( 'NONE', *, *, #21125, .T. ) ;
#23110=SURFACE_STYLE_USAGE ( .BOTH. , #13460 ) ;
#23171=ORIENTED_EDGE ( 'NONE', *, *, #1265, .F. ) ;
#23395=ORIENTED_EDGE ( 'NONE', *, *, #39804, .F. ) ;
#23418=ORIENTED_EDGE ( 'NONE', *, *, #43916, .T. ) ;
#23656=VERTEX_POINT ( 'NONE', #44993 ) ;
#23698=CARTESIAN_POINT ( 'NONE',  ( -6.293430271071534854, 5.026740376715094882, -0.4524126574264483169 ) ) ;
#23938=ORIENTED_EDGE ( 'NONE', *, *, #5823, .F. ) ;
#24006=CARTESIAN_POINT ( 'NONE',  ( 0.000000000000000000, 0.000000000000000000, -0.5251556536572846712 ) ) ;
#24066=AXIS2_PLACEMENT_3D ( 'NONE', #39918, #34144, #19672 ) ;
#24098=CARTESIAN_POINT ( 'NONE',  ( 0.04725809328185039127, -9.175759667312528123, -8.057670357645362103 ) ) ;
#24157=EDGE_LOOP ( 'NONE', ( #38819, #51675, #51875, #63652, #6605 ) ) ;
#24198=ORIENTED_EDGE ( 'NONE', *, *, #9399, .T. ) ;
#24260=CARTESIAN_POINT ( 'NONE',  ( -6.127431526422343306E-17, 9.147862274876549904, -8.047472243342932430 ) ) ;
#24293=CARTESIAN_POINT ( 'NONE',  ( -7.808218555863073007, -4.508077085118257443, -7.999534413642739317 ) ) ;
#24331=B_SPLINE_CURVE_WITH_KNOTS ( 'NONE', 3,
 ( #31824, #2262, #2890, #32452, #22502, #56280, #31494, #42412, #52084, #21865 ),
 .UNSPECIFIED., .F., .F.,
 ( 4, 2, 2, 2, 4 ),
 ( 0.01051144076094934904, 0.01162027323572610918, 0.01272910571050286932, 0.01383793818527962946, 0.01494677066005638960 ),
 .UNSPECIFIED. ) ;
#24352=VERTEX_POINT ( 'NONE', #27126 ) ;
#24354=FACE_OUTER_BOUND ( 'NONE', #56287, .T. ) ;
#24370=CARTESIAN_POINT ( 'NONE',  ( -7.499999999999653610, -1.545780083834116247, -7.491787297939224821 ) ) ;
#24371=DIRECTION ( 'NONE',  ( 0.000000000000000000, 0.000000000000000000, 1.000000000000000000 ) ) ;
#24374=CIRCLE ( 'NONE', #61363, 10.12668159690567649 ) ;
#24596=( GEOMETRIC_REPRESENTATION_CONTEXT ( 3 ) GLOBAL_UNCERTAINTY_ASSIGNED_CONTEXT ( ( #48711 ) ) GLOBAL_UNIT_ASSIGNED_CONTEXT ( ( #61097, #51123, #56901 ) ) REPRESENTATION_CONTEXT ( 'NONE', 'WORKASPACE' ) );
#24630=CARTESIAN_POINT ( 'NONE',  ( -7.897836333153808397, -1.530409084195006653, -7.633857274177628938 ) ) ;
#24644=CARTESIAN_POINT ( 'NONE',  ( -1.015826369459165157, 8.073766409993364590, -7.642786413619490737 ) ) ;
#24645=CARTESIAN_POINT ( 'NONE',  ( -3.288228914120473245, 7.217643567644804747, -7.591235721156635030 ) ) ;
#24648=AXIS2_PLACEMENT_3D ( 'NONE', #14833, #44103, #10017 ) ;
#24682=ORIENTED_EDGE ( 'NONE', *, *, #36274, .T. ) ;
#24762=CARTESIAN_POINT ( 'NONE',  ( -3.750000000000007105, -6.495190528383289141, 0.000000000000000000 ) ) ;
#24789=CARTESIAN_POINT ( 'NONE',  ( -5.007715329123872641E-16, -8.660254037844399733, -7.422398894150038728 ) ) ;
#24794=AXIS2_PLACEMENT_3D ( 'NONE', #26910, #46529, #51674 ) ;
#24842=ADVANCED_FACE ( 'NONE', ( #56965 ), #62815, .T. ) ;
#24888=DIRECTION ( 'NONE',  ( -1.000000000000000000, 0.000000000000000000, 0.000000000000000000 ) ) ;
#24902=PRODUCT_DEFINITION ( 'UNKNOWN', '', #48237, #39061 ) ;
#24950=CARTESIAN_POINT ( 'NONE',  ( 10.12668159690567649, 0.000000000000000000, -9.999999999999998224 ) ) ;
#25007=CARTESIAN_POINT ( 'NONE',  ( -7.500000000000000000, -0.7729939684941458111, -7.026407045654831762 ) ) ;
#25054=B_SPLINE_CURVE_WITH_KNOTS ( 'NONE', 3,
 ( #51273, #32908, #52531, #46437, #32586, #16841 ),
 .UNSPECIFIED., .F., .F.,
 ( 4, 2, 4 ),
 ( 0.000000000000000000, 0.0004189869898913735043, 0.0008379739797827470086 ),
 .UNSPECIFIED. ) ;
#25058=ORIENTED_EDGE ( 'NONE', *, *, #38230, .T. ) ;
#25153=ORIENTED_EDGE ( 'NONE', *, *, #35914, .T. ) ;
#25192=CARTESIAN_POINT ( 'NONE',  ( -0.6249999999999991118, -8.299410119600880265, -7.298562697733108173 ) ) ;
#25214=CARTESIAN_POINT ( 'NONE',  ( 5.047120108843200725, -5.746297884371399434, -0.1007566405101860824 ) ) ;
#25223=ADVANCED_FACE ( 'NONE', ( #24354 ), #48787, .T. ) ;
#25293=CONICAL_SURFACE ( 'NONE', #31442, 7.500000000000001776, 0.8594454914424796144 ) ;
#25397=AXIS2_PLACEMENT_3D ( 'NONE', #47172, #3116, #22734 ) ;
#25466=ORIENTED_EDGE ( 'NONE', *, *, #5182, .T. ) ;
#25531=CARTESIAN_POINT ( 'NONE',  ( 7.500000000000000000, 3.948247735265829395, -7.349893093595813554 ) ) ;
#25610=CARTESIAN_POINT ( 'NONE',  ( -6.288404560131954923, -5.029641972278938944, -0.4504974108212008721 ) ) ;
#25660=EDGE_CURVE ( 'NONE', #40464, #31318, #25803, .T. ) ;
#25737=CARTESIAN_POINT ( 'NONE',  ( 7.848314987057850800, -4.129027267381569999, -7.493854785173811095 ) ) ;
#25803=CIRCLE ( 'NONE', #46374, 7.500000000000001776 ) ;
#25848=EDGE_CURVE ( 'NONE', #50923, #38994, #31555, .T. ) ;
#25851=CARTESIAN_POINT ( 'NONE',  ( 7.500000000000000000, 0.7723602884954153813, -7.026388801733942202 ) ) ;
#25918=CARTESIAN_POINT ( 'NONE',  ( -7.298354728638373423, 4.926141412641537265, -7.913704048100170141 ) ) ;
#26038=DIRECTION ( 'NONE',  ( 0.5000000000000006661, 0.8660254037844383745, -0.000000000000000000 ) ) ;
#26041=CARTESIAN_POINT ( 'NONE',  ( -1.206569728928481577, -7.963640680051488729, -0.4524126574264552558 ) ) ;
#26047=EDGE_LOOP ( 'NONE', ( #14787, #55872, #62002 ) ) ;
#26054=CARTESIAN_POINT ( 'NONE',  ( 5.112021521198788498, -5.708827036477115868, -7.069802615102037890 ) ) ;
#26061=CARTESIAN_POINT ( 'NONE',  ( 7.499999999999999112, 1.854554393013827296, -0.1880126015361732184 ) ) ;
#26083=CARTESIAN_POINT ( 'NONE',  ( 7.922281120364393914, -4.573931137438282057, -8.047472243342932430 ) ) ;
#26091=CONICAL_SURFACE ( 'NONE', #7648, 4.174999999999999822, 0.9599310885968795892 ) ;
#26155=CARTESIAN_POINT ( 'NONE',  ( -6.658902113226115027, -5.287118297636088649, -7.776713651266535798 ) ) ;
#26201=CARTESIAN_POINT ( 'NONE',  ( 7.500000000000000888, 3.608439182435154269, -7.298562697733103732 ) ) ;
#26290=VERTEX_POINT ( 'NONE', #43440 ) ;
#26301=EDGE_CURVE ( 'NONE', #3756, #23656, #22337, .T. ) ;
#26375=CARTESIAN_POINT ( 'NONE',  ( 7.499999999999999112, 0.3744244963005059490, 1.526918059583750369E-15 ) ) ;
#26443=EDGE_CURVE ( 'NONE', #727, #22221, #20033, .T. ) ;
#26477=CARTESIAN_POINT ( 'NONE',  ( -6.484173630544109557, -4.916614646775610886, -7.642786413610934915 ) ) ;
#26514=CARTESIAN_POINT ( 'NONE',  ( 2.621086668468698644, 7.606368536631364030, -7.634085501268425666 ) ) ;
#26690=CARTESIAN_POINT ( 'NONE',  ( 7.500000000000000000, 4.330127018922190096, -7.422398894150032511 ) ) ;
#26691=CARTESIAN_POINT ( 'NONE',  ( 5.088535779737119569, -5.722386535631984295, -7.491772860715834703 ) ) ;
#26753=CARTESIAN_POINT ( 'NONE',  ( -3.750000000000001776, 6.495190528383289141, -6.991905250253753756 ) ) ;
#26790=CARTESIAN_POINT ( 'NONE',  ( 7.894787914004607998, 1.243647571710251278E-13, -7.591390474663425536 ) ) ;
#26793=CARTESIAN_POINT ( 'NONE',  ( -3.295171437451516638, -7.213553046160524396, -7.590212325761481971 ) ) ;
#26804=CARTESIAN_POINT ( 'NONE',  ( 7.500000000000000000, -1.645076096015019695, -7.030022527230891605 ) ) ;
#26852=CARTESIAN_POINT ( 'NONE',  ( -0.04725809328185606034, 9.175759667312519241, -8.057670357645360326 ) ) ;
#26862=ORIENTED_EDGE ( 'NONE', *, *, #50427, .F. ) ;
#26884=CARTESIAN_POINT ( 'NONE',  ( 7.500000000000000000, 4.330127018922199866, -1.000000000000000888 ) ) ;
#26910=CARTESIAN_POINT ( 'NONE',  ( -14.99999999999998934, -1.734723475976807094E-15, -10.00000000000000000 ) ) ;
#27087=CARTESIAN_POINT ( 'NONE',  ( 4.403473400622098133, 6.117907484625861869, 2.043043468777371629E-15 ) ) ;
#27126=CARTESIAN_POINT ( 'NONE',  ( 10.39117206796836257, 0.000000000000000000, -8.499999999999998224 ) ) ;
#27205=CARTESIAN_POINT ( 'NONE',  ( -7.500000000000000888, -3.640541674360520119, -0.7158139487964623182 ) ) ;
#27221=EDGE_LOOP ( 'NONE', ( #59982, #13140, #33516, #32280, #62733 ) ) ;
#27236=CIRCLE ( 'NONE', #63192, 7.500000000000001776 ) ;
#27317=CARTESIAN_POINT ( 'NONE',  ( 7.703928834700296768, 4.447865386531931975, -7.917997657324726823 ) ) ;
#27372=CARTESIAN_POINT ( 'NONE',  ( -0.6250000000000001110, 8.299410119600874935, -7.298562697733108173 ) ) ;
#27458=VECTOR ( 'NONE', #44385, 1000.000000000000000 ) ;
#27460=CARTESIAN_POINT ( 'NONE',  ( 4.336808689942017736E-16, 8.660254037844390851, -1.000000000000000888 ) ) ;
#27622=DIRECTION ( 'NONE',  ( -0.5000000000000005551, 0.8660254037844383745, 0.000000000000000000 ) ) ;
#27726=CIRCLE ( 'NONE', #59602, 5.000000000000000888 ) ;
#27772=CIRCLE ( 'NONE', #59650, 5.000000000000001776 ) ;
#27776=CARTESIAN_POINT ( 'NONE',  ( 0.5984201754795568373, 8.314755988442765755, -0.7022220667781353676 ) ) ;
#27901=EDGE_LOOP ( 'NONE', ( #23171, #24198, #6231, #36704, #13203 ) ) ;
#27925=( LENGTH_UNIT ( ) NAMED_UNIT ( * ) SI_UNIT ( .MILLI., .METRE. ) );
#28038=DIRECTION ( 'NONE',  ( -0.000000000000000000, -0.000000000000000000, 1.000000000000000000 ) ) ;
#28073=CARTESIAN_POINT ( 'NONE',  ( -5.007715329123872641E-16, -8.660254037844399733, -7.422398894150038728 ) ) ;
#28175=CARTESIAN_POINT ( 'NONE',  ( -7.922281120364393914, -4.573931137438277617, -8.047472243342932430 ) ) ;
#28261=CARTESIAN_POINT ( 'NONE',  ( 0.000000000000000000, 0.000000000000000000, -9.999999999999998224 ) ) ;
#28285=ADVANCED_FACE ( 'NONE', ( #126 ), #1407, .F. ) ;
#28326=ADVANCED_FACE ( 'NONE', ( #2658 ), #7173, .F. ) ;
#28336=ORIENTED_EDGE ( 'NONE', *, *, #41666, .F. ) ;
#28522=CARTESIAN_POINT ( 'NONE',  ( -4.613983237546153582, 6.452243898629808960, -7.591546097228401457 ) ) ;
#28539=VERTEX_POINT ( 'NONE', #17762 ) ;
#28613=ORIENTED_EDGE ( 'NONE', *, *, #9964, .T. ) ;
#28615=ADVANCED_FACE ( 'NONE', ( #33500 ), #52805, .T. ) ;
#28649=CARTESIAN_POINT ( 'NONE',  ( -1.994931997373328159E-14, -8.660254037844390851, -1.000000000000000888 ) ) ;
#28689=EDGE_CURVE ( 'NONE', #41293, #21365, #52175, .T. ) ;
#28774=AXIS2_PLACEMENT_3D ( 'NONE', #47665, #18399, #63104 ) ;
#28775=B_SPLINE_CURVE_WITH_KNOTS ( 'NONE', 3,
 ( #5263, #44484, #30328, #20704, #15555, #49319, #35810, #25192, #10077 ),
 .UNSPECIFIED., .F., .F.,
 ( 4, 2, 1, 2, 4 ),
 ( 0.000000000000000000, 0.002165063509461097064, 0.004330127018922194128, 0.006495190528383290758, 0.008660254037844389990 ),
 .UNSPECIFIED. ) ;
#28789=ORIENTED_EDGE ( 'NONE', *, *, #44151, .T. ) ;
#28804=CARTESIAN_POINT ( 'NONE',  ( -7.703920929261744988, -4.447860822324864571, -7.917989418073275942 ) ) ;
#28842=EDGE_LOOP ( 'NONE', ( #30150, #17143 ) ) ;
#28898=EDGE_CURVE ( 'NONE', #29821, #1507, #61371, .T. ) ;
#29058=VERTEX_POINT ( 'NONE', #9828 ) ;
#29083=ORIENTED_EDGE ( 'NONE', *, *, #50427, .T. ) ;
#29121=CARTESIAN_POINT ( 'NONE',  ( -7.894787914004607998, -1.230850257101226302E-13, -7.591390474663425536 ) ) ;
#29267=CARTESIAN_POINT ( 'NONE',  ( 5.276765049035074817, -6.073111908730307817, -7.634085501268428331 ) ) ;
#29373=EDGE_CURVE ( 'NONE', #29058, #32825, #42344, .T. ) ;
#29399=ORIENTED_EDGE ( 'NONE', *, *, #38067, .F. ) ;
#29407=DIRECTION ( 'NONE',  ( 0.000000000000000000, 0.000000000000000000, -1.000000000000000000 ) ) ;
#29492=CARTESIAN_POINT ( 'NONE',  ( -7.500000000000000000, -1.572902445675612659, -7.069816568113127531 ) ) ;
#29493=B_SPLINE_CURVE_WITH_KNOTS ( 'NONE', 3,
 ( #12977, #47396, #18120, #26514, #56105, #12026, #31655, #22008, #51290, #41602 ),
 .UNSPECIFIED., .F., .F.,
 ( 4, 2, 2, 2, 4 ),
 ( 1.572453990175171705E-19, 0.002305503304226491201, 0.004611006608452982401, 0.006916509912679473168, 0.009222013216905964803 ),
 .UNSPECIFIED. ) ;
#29507=CARTESIAN_POINT ( 'NONE',  ( -7.922281120364393914, -4.573931137438277617, -8.047472243342932430 ) ) ;
#29591=CARTESIAN_POINT ( 'NONE',  ( 1.305263714129178743, -8.377797850839291627, -7.792447862505339273 ) ) ;
#29643=AXIS2_PLACEMENT_3D ( 'NONE', #47383, #12009, #7521 ) ;
#29763=DIRECTION ( 'NONE',  ( 0.000000000000000000, 0.000000000000000000, 1.000000000000000000 ) ) ;
#29797=APPLICATION_CONTEXT ( 'automotive_design' ) ;
#29821=VERTEX_POINT ( 'NONE', #58659 ) ;
#29980=CARTESIAN_POINT ( 'NONE',  ( 0.000000000000000000, 0.000000000000000000, -10.00000000000000000 ) ) ;
#29985=VERTEX_POINT ( 'NONE', #14902 ) ;
#30042=EDGE_LOOP ( 'NONE', ( #54996, #60951, #30051 ) ) ;
#30051=ORIENTED_EDGE ( 'NONE', *, *, #44444, .F. ) ;
#30093=FACE_OUTER_BOUND ( 'NONE', #30103, .T. ) ;
#30103=EDGE_LOOP ( 'NONE', ( #18894, #48249, #39525, #31657 ) ) ;
#30135=FACE_OUTER_BOUND ( 'NONE', #41057, .T. ) ;
#30150=ORIENTED_EDGE ( 'NONE', *, *, #39788, .F. ) ;
#30209=CARTESIAN_POINT ( 'NONE',  ( -1.994931997373328159E-14, -8.660254037844390851, -1.000000000000000888 ) ) ;
#30234=CARTESIAN_POINT ( 'NONE',  ( -7.500000000000000000, 4.330127018922191873, -7.422398894150032511 ) ) ;
#30285=EDGE_LOOP ( 'NONE', ( #35610, #19235, #50545 ) ) ;
#30328=CARTESIAN_POINT ( 'NONE',  ( -6.250000000000000000, -5.051814855409233473, -7.198902722707430257 ) ) ;
#30429=ORIENTED_EDGE ( 'NONE', *, *, #20933, .F. ) ;
#30539=CARTESIAN_POINT ( 'NONE',  ( 7.922281120364393914, 4.573931137438269623, -8.047472243342930653 ) ) ;
#30568=DIRECTION ( 'NONE',  ( 0.000000000000000000, 0.000000000000000000, -1.000000000000000000 ) ) ;
#30571=CIRCLE ( 'NONE', #57321, 10.12668159690567649 ) ;
#30675=CARTESIAN_POINT ( 'NONE',  ( 7.499999999998625100, 3.882635837268474166, -7.781684861371460649 ) ) ;
#30808=AXIS2_PLACEMENT_3D ( 'NONE', #13897, #58598, #14518 ) ;
#30885=CARTESIAN_POINT ( 'NONE',  ( -7.549004593702452581, 4.358419834287830419, -7.700121441565820568 ) ) ;
#30891=AXIS2_PLACEMENT_3D ( 'NONE', #59938, #5569, #15860 ) ;
#30954=( BOUNDED_SURFACE ( )  B_SPLINE_SURFACE ( 3, 2, ( 
 ( #49126, #15677, #34019 ),
 ( #35296, #49449, #14396 ),
 ( #5391, #34652, #4746 ),
 ( #25007, #44616, #576 ),
 ( #29492, #24370, #53640 ),
 ( #1228, #14709, #39784 ),
 ( #10843, #20185, #9573 ),
 ( #20512, #54917, #5068 ) ),
 .UNSPECIFIED., .F., .F., .F. ) 
 B_SPLINE_SURFACE_WITH_KNOTS ( ( 4, 2, 2, 4 ),
 ( 3, 3 ),
 ( 0.03851319102641418551, 0.04314724750133520914, 0.04546427573879571749, 0.04778130397625623277 ),
 ( 0.000000000000000000, 1.000000000000000000 ),
 .UNSPECIFIED. ) 
 GEOMETRIC_REPRESENTATION_ITEM ( )  RATIONAL_B_SPLINE_SURFACE ( (
 ( 1.000000000000000000, 0.8047781573724569482, 1.000000000000000000),
 ( 1.000000000000000000, 0.8123768202405010630, 1.000000000000000000),
 ( 1.000000000000000000, 0.8190667609311549358, 1.000000000000000000),
 ( 1.000000000000000000, 0.8191933927154739781, 1.000000000000000000),
 ( 1.000000000000000000, 0.8176088169850088683, 1.000000000000000000),
 ( 1.000000000000000000, 0.8122958474542694152, 1.000000000000000000),
 ( 1.000000000000000000, 0.8086309703845098174, 1.000000000000000000),
 ( 1.000000000000000000, 0.8047712409910821041, 1.000000000000000000) ) ) 
 REPRESENTATION_ITEM ( '' )  SURFACE ( )  );
#31026=ADVANCED_FACE ( 'NONE', ( #59030 ), #19469, .T. ) ;
#31285=CARTESIAN_POINT ( 'NONE',  ( -0.3306966981848578069, -8.469326210127253063, -7.349897473154448413 ) ) ;
#31316=ORIENTED_EDGE ( 'NONE', *, *, #63608, .F. ) ;
#31318=VERTEX_POINT ( 'NONE', #59352 ) ;
#31336=CARTESIAN_POINT ( 'NONE',  ( 1.060314165522845187, 8.048081368953960535, -7.659344964963204383 ) ) ;
#31364=ORIENTED_EDGE ( 'NONE', *, *, #20854, .T. ) ;
#31385=EDGE_CURVE ( 'NONE', #1507, #40464, #12179, .T. ) ;
#31442=AXIS2_PLACEMENT_3D ( 'NONE', #38042, #58294, #3953 ) ;
#31488=AXIS2_PLACEMENT_3D ( 'NONE', #12723, #47143, #3090 ) ;
#31494=CARTESIAN_POINT ( 'NONE',  ( -7.500000000000001776, 2.932633423934442263, -0.4709827563909292358 ) ) ;
#31535=CARTESIAN_POINT ( 'NONE',  ( 7.500000000000006217, -4.330127018922195425, -7.564338275809326717 ) ) ;
#31541=AXIS2_PLACEMENT_3D ( 'NONE', #40855, #30568, #11590 ) ;
#31555=B_SPLINE_CURVE_WITH_KNOTS ( 'NONE', 3,
 ( #28175, #24293, #28804, #47482, #13700, #43897 ),
 .UNSPECIFIED., .F., .F.,
 ( 4, 2, 4 ),
 ( -5.145455527293010977E-06, 0.0004153350442917510058, 0.0008358155441107968436 ),
 .UNSPECIFIED. ) ;
#31655=CARTESIAN_POINT ( 'NONE',  ( 5.274401269815139237, 6.074457022762083547, -7.633824513837111247 ) ) ;
#31657=ORIENTED_EDGE ( 'NONE', *, *, #11751, .F. ) ;
#31666=CARTESIAN_POINT ( 'NONE',  ( 1.013163106016871096, 8.075304045852551127, -7.231838333420561149 ) ) ;
#31710=CARTESIAN_POINT ( 'NONE',  ( -7.499999999999999112, -2.930060224340425901, -0.4701183149080249146 ) ) ;
#31722=AXIS2_PLACEMENT_3D ( 'NONE', #46506, #50049, #40708 ) ;
#31814=STYLED_ITEM ( 'NONE', ( #13763 ), #57040 ) ;
#31824=CARTESIAN_POINT ( 'NONE',  ( -7.500000000000001776, 0.000000000000000000, 0.000000000000000000 ) ) ;
#31828=CARTESIAN_POINT ( 'NONE',  ( -0.3470952277635217520, -8.860649561028104415, -7.493596212620245112 ) ) ;
#31831=ORIENTED_EDGE ( 'NONE', *, *, #38230, .F. ) ;
#31837=DIRECTION ( 'NONE',  ( 0.000000000000000000, -1.000000000000000000, 0.000000000000000000 ) ) ;
#31873=CARTESIAN_POINT ( 'NONE',  ( 0.000000000000000000, 0.000000000000000000, 0.000000000000000000 ) ) ;
#31888=CARTESIAN_POINT ( 'NONE',  ( -5.000000000000000888, 5.773502691896258199, -7.063244554130002406 ) ) ;
#32138=EDGE_LOOP ( 'NONE', ( #34409, #8014, #60230, #12325, #53633 ) ) ;
#32279=DIRECTION ( 'NONE',  ( 0.000000000000000000, 0.000000000000000000, -1.000000000000000000 ) ) ;
#32280=ORIENTED_EDGE ( 'NONE', *, *, #47658, .T. ) ;
#32344=CARTESIAN_POINT ( 'NONE',  ( -7.500000000000000000, -1.486698507076798847, -0.09861472150523968583 ) ) ;
#32345=ORIENTED_EDGE ( 'NONE', *, *, #46840, .F. ) ;
#32358=FACE_OUTER_BOUND ( 'NONE', #30042, .T. ) ;
#32452=CARTESIAN_POINT ( 'NONE',  ( -7.499999999999998224, 1.489914625143999416, -0.1187923833806747292 ) ) ;
#32467=DIRECTION ( 'NONE',  ( 0.000000000000000000, 0.000000000000000000, -1.000000000000000000 ) ) ;
#32512=AXIS2_PLACEMENT_3D ( 'NONE', #61441, #31837, #32467 ) ;
#32579=LINE ( 'NONE', #42226, #62548 ) ;
#32586=CARTESIAN_POINT ( 'NONE',  ( -4.229293425455167136E-15, -9.016621985895922009, -7.999704684617492845 ) ) ;
#32598=ORIENTED_EDGE ( 'NONE', *, *, #44055, .T. ) ;
#32619=EDGE_CURVE ( 'NONE', #35203, #4851, #41569, .T. ) ;
#32745=CARTESIAN_POINT ( 'NONE',  ( -7.500000000000000000, 4.330127018922191873, -10.00000000000000000 ) ) ;
#32789=AXIS2_PLACEMENT_3D ( 'NONE', #1133, #55784, #56100 ) ;
#32825=VERTEX_POINT ( 'NONE', #51783 ) ;
#32908=CARTESIAN_POINT ( 'NONE',  ( -3.823040241140506157E-16, -8.660254037844399733, -7.564338275809332046 ) ) ;
#32933=EDGE_LOOP ( 'NONE', ( #11623, #52347, #10199, #23395 ) ) ;
#32969=LINE ( 'NONE', #13031, #35036 ) ;
#33049=ADVANCED_FACE ( 'NONE', ( #39460, #59095 ), #46206, .F. ) ;
#33125=CARTESIAN_POINT ( 'NONE',  ( 0.2791032213812723040, -8.821394357840571132, -7.929128246061910801 ) ) ;
#33233=DIRECTION ( 'NONE',  ( -1.000000000000000000, 0.000000000000000000, 0.000000000000000000 ) ) ;
#33257=DIRECTION ( 'NONE',  ( -0.000000000000000000, -0.000000000000000000, 1.000000000000000000 ) ) ;
#33486=DIRECTION ( 'NONE',  ( 1.000000000000000000, 0.000000000000000000, 0.000000000000000000 ) ) ;
#33500=FACE_OUTER_BOUND ( 'NONE', #24157, .T. ) ;
#33516=ORIENTED_EDGE ( 'NONE', *, *, #40875, .T. ) ;
#33636=DIRECTION ( 'NONE',  ( 1.000000000000000000, 0.000000000000000000, 0.000000000000000000 ) ) ;
#33827=CONICAL_SURFACE ( 'NONE', #61582, 5.000000000000001776, 0.9599310885968795892 ) ;
#33850=ORIENTED_EDGE ( 'NONE', *, *, #59513, .F. ) ;
#33926=UNCERTAINTY_MEASURE_WITH_UNIT (LENGTH_MEASURE( 1.000000000000000082E-05 ), #27925, 'distance_accuracy_value', 'NONE');
#33977=CARTESIAN_POINT ( 'NONE',  ( 0.3470952277635277472, 8.860649561028097310, -7.493596212620242447 ) ) ;
#34019=CARTESIAN_POINT ( 'NONE',  ( -7.922798540899431252, 4.627424769998836673, -8.057412477672047046 ) ) ;
#34102=CARTESIAN_POINT ( 'NONE',  ( 10.39117206796836079, 1.272551561242683567E-15, -8.499999999999998224 ) ) ;
#34103=CARTESIAN_POINT ( 'NONE',  ( 2.623433461001182909, -7.604994000793866782, -7.633824513837117465 ) ) ;
#34112=CARTESIAN_POINT ( 'NONE',  ( 7.500000000000000000, -4.330127018922199866, -7.422398894150035176 ) ) ;
#34144=DIRECTION ( 'NONE',  ( -0.000000000000000000, -0.000000000000000000, 1.000000000000000000 ) ) ;
#34240=ORIENTED_EDGE ( 'NONE', *, *, #21125, .F. ) ;
#34257=ADVANCED_FACE ( 'NONE', ( #36635 ), #1610, .T. ) ;
#34275=CARTESIAN_POINT ( 'NONE',  ( -7.500000000000000000, -4.330127018922198090, -10.00000000000000000 ) ) ;
#34409=ORIENTED_EDGE ( 'NONE', *, *, #42806, .F. ) ;
#34451=DIRECTION ( 'NONE',  ( -0.9396926207859143121, 0.000000000000000000, -0.3420201433256525592 ) ) ;
#34517=ORIENTED_EDGE ( 'NONE', *, *, #20854, .F. ) ;
#34526=CARTESIAN_POINT ( 'NONE',  ( -2.352990130084580066E-16, 8.660254037844390851, -7.422398894150034288 ) ) ;
#34544=CARTESIAN_POINT ( 'NONE',  ( 0.000000000000000000, 0.000000000000000000, -0.5776712190230133270 ) ) ;
#34598=CARTESIAN_POINT ( 'NONE',  ( -6.439685834476978954, 4.942299687812971243, -7.659344964963200830 ) ) ;
#34652=CARTESIAN_POINT ( 'NONE',  ( -7.500000000000698996, 1.613867362005801054, -7.450195926347907616 ) ) ;
#34709=CARTESIAN_POINT ( 'NONE',  ( -10.12668159690567649, 1.240160820363494356E-15, -9.226681596905677907 ) ) ;
#34752=CARTESIAN_POINT ( 'NONE',  ( 7.500000000000002665, 3.988838049906435312, -0.8529248949437669980 ) ) ;
#34997=CARTESIAN_POINT ( 'NONE',  ( -7.263825692932299738, -4.945657111639584436, -7.907570769506049757 ) ) ;
#35036=VECTOR ( 'NONE', #62251, 1000.000000000000114 ) ;
#35058=CARTESIAN_POINT ( 'NONE',  ( -7.500000000000000000, -4.330127018922199866, -1.000000000000000888 ) ) ;
#35076=CARTESIAN_POINT ( 'NONE',  ( 7.499999999999999112, 0.7513028741560161539, -0.02472015219302839059 ) ) ;
#35203=VERTEX_POINT ( 'NONE', #20340 ) ;
#35259=CYLINDRICAL_SURFACE ( 'NONE', #31722, 5.000000000000000888 ) ;
#35296=CARTESIAN_POINT ( 'NONE',  ( -7.500000000000000000, 3.202583086485915942, -7.213046687579523386 ) ) ;
#35537=CARTESIAN_POINT ( 'NONE',  ( 7.500000000000000888, -2.886751345948134873, -7.198902722707428481 ) ) ;
#35581=CARTESIAN_POINT ( 'NONE',  ( -3.750000000000007105, -6.495190528383289141, 0.000000000000000000 ) ) ;
#35610=ORIENTED_EDGE ( 'NONE', *, *, #31385, .T. ) ;
#35706=CARTESIAN_POINT ( 'NONE',  ( 4.406466114817131796, -6.116179640279303165, -7.446478553994418270 ) ) ;
#35713=DIRECTION ( 'NONE',  ( -0.000000000000000000, -0.000000000000000000, 1.000000000000000000 ) ) ;
#35730=EDGE_CURVE ( 'NONE', #63287, #35203, #47613, .T. ) ;
#35810=CARTESIAN_POINT ( 'NONE',  ( -1.250000000000000444, -7.938566201357367902, -7.198902722707430257 ) ) ;
#35914=EDGE_CURVE ( 'NONE', #48710, #40464, #18816, .T. ) ;
#36045=FACE_OUTER_BOUND ( 'NONE', #26047, .T. ) ;
#36055=CARTESIAN_POINT ( 'NONE',  ( 7.549006887134058985, -4.358421158401196926, -7.700127545397296380 ) ) ;
#36069=VERTEX_POINT ( 'NONE', #30539 ) ;
#36086=AXIS2_PLACEMENT_3D ( 'NONE', #31873, #18023, #12259 ) ;
#36090=ORIENTED_EDGE ( 'NONE', *, *, #63608, .T. ) ;
#36127=CARTESIAN_POINT ( 'NONE',  ( -1.013163106016700565, -8.075304045852661261, -7.231838333420565590 ) ) ;
#36195=ORIENTED_EDGE ( 'NONE', *, *, #2418, .F. ) ;
#36270=CARTESIAN_POINT ( 'NONE',  ( 0.000000000000000000, 0.000000000000000000, -8.499999999999998224 ) ) ;
#36274=EDGE_CURVE ( 'NONE', #49290, #21365, #48497, .T. ) ;
#36284=CARTESIAN_POINT ( 'NONE',  ( 0.000000000000000000, 0.000000000000000000, 0.000000000000000000 ) ) ;
#36348=ADVANCED_FACE ( 'NONE', ( #48182 ), #53327, .T. ) ;
#36396=CARTESIAN_POINT ( 'NONE',  ( -2.352990130084580066E-16, 8.660254037844390851, -7.422398894150034288 ) ) ;
#36406=DIRECTION ( 'NONE',  ( -0.000000000000000000, -0.000000000000000000, 1.000000000000000000 ) ) ;
#36439=CARTESIAN_POINT ( 'NONE',  ( -2.387978478801491278, -7.281554020289322970, -7.069802615102039667 ) ) ;
#36453=FACE_OUTER_BOUND ( 'NONE', #59446, .T. ) ;
#36604=EDGE_CURVE ( 'NONE', #13010, #49422, #63299, .T. ) ;
#36605=ADVANCED_FACE ( 'NONE', ( #30135 ), #30954, .F. ) ;
#36631=LINE ( 'NONE', #40496, #40543 ) ;
#36635=FACE_OUTER_BOUND ( 'NONE', #32138, .T. ) ;
#36696=STYLED_ITEM('',(#63719),#50087);
#36704=ORIENTED_EDGE ( 'NONE', *, *, #15780, .T. ) ;
#36742=CARTESIAN_POINT ( 'NONE',  ( 6.288404560131952259, 5.029641972278931839, -0.4504974108211943773 ) ) ;
#36795=ORIENTED_EDGE ( 'NONE', *, *, #39788, .T. ) ;
#36978=CARTESIAN_POINT ( 'NONE',  ( -0.2779000157839473517, -8.820699686765063774, -7.928862157988305626 ) ) ;
#36986=CARTESIAN_POINT ( 'NONE',  ( -7.500000000000000000, 4.330127018922191873, -7.422398894150032511 ) ) ;
#37232=DIRECTION ( 'NONE',  ( -1.000000000000000000, 0.000000000000000000, 0.000000000000000000 ) ) ;
#37438=CARTESIAN_POINT ( 'NONE',  ( 3.093157300003884558, 6.874418838041288282, 2.127746763502802452E-15 ) ) ;
#37486=CARTESIAN_POINT ( 'NONE',  ( -7.500000000000001776, 0.000000000000000000, 0.000000000000000000 ) ) ;
#37537=B_SPLINE_CURVE_WITH_KNOTS ( 'NONE', 3,
 ( #30209, #50490, #26041, #45656, #5143, #24762 ),
 .UNSPECIFIED., .F., .F.,
 ( 4, 2, 4 ),
 ( 2.475503369438313607E-07, 0.002222330217055647119, 0.004444412883774350592 ),
 .UNSPECIFIED. ) ;
#37608=TOROIDAL_SURFACE ( 'NONE', #47880, 10.12668159690567649, 0.7733184030943209830 ) ;
#37707=VERTEX_POINT ( 'NONE', #48257 ) ;
#37742=CARTESIAN_POINT ( 'NONE',  ( 7.907996613752301229, 3.055722423191984838, -7.792112796859423263 ) ) ;
#38042=CARTESIAN_POINT ( 'NONE',  ( 0.000000000000000000, 0.000000000000000000, 0.000000000000000000 ) ) ;
#38067=EDGE_CURVE ( 'NONE', #727, #36069, #41336, .T. ) ;
#38223=SHAPE_REPRESENTATION_RELATIONSHIP ( 'NONE' , 'NONE' ,  #14320, #57040 ) ;
#38230=EDGE_CURVE ( 'NONE', #41293, #63519, #18910, .T. ) ;
#38331=DIRECTION ( 'NONE',  ( -0.8191520442889907994, 1.003171929053523514E-16, 0.5735764363510474917 ) ) ;
#38367=DIRECTION ( 'NONE',  ( 0.000000000000000000, 0.000000000000000000, 1.000000000000000000 ) ) ;
#38425=ORIENTED_EDGE ( 'NONE', *, *, #12931, .T. ) ;
#38429=CARTESIAN_POINT ( 'NONE',  ( 0.000000000000000000, 0.000000000000000000, -8.499999999999998224 ) ) ;
#38466=CIRCLE ( 'NONE', #24066, 5.000000000000000888 ) ;
#38709=DIRECTION ( 'NONE',  ( 0.000000000000000000, 0.000000000000000000, 1.000000000000000000 ) ) ;
#38723=CARTESIAN_POINT ( 'NONE',  ( 6.901579824520443829, -4.675625068323827627, -0.7022220667781372549 ) ) ;
#38819=ORIENTED_EDGE ( 'NONE', *, *, #36604, .F. ) ;
#38821=ADVANCED_FACE ( 'NONE', ( #11383 ), #26091, .F. ) ;
#38830=ORIENTED_EDGE ( 'NONE', *, *, #62480, .T. ) ;
#38994=VERTEX_POINT ( 'NONE', #57685 ) ;
#39046=CARTESIAN_POINT ( 'NONE',  ( -2.352990130084580066E-16, 8.660254037844390851, -7.564335161054483336 ) ) ;
#39061=PRODUCT_DEFINITION_CONTEXT ( 'detailed design', #242, 'design' ) ;
#39110=CARTESIAN_POINT ( 'NONE',  ( -4.419133455862249704, 6.108866147517435508, -7.026396753507433424 ) ) ;
#39167=CARTESIAN_POINT ( 'NONE',  ( -2.621086668468698644, -7.606368536631371136, -7.634085501268427443 ) ) ;
#39197=DIRECTION ( 'NONE',  ( -0.000000000000000000, -0.000000000000000000, 1.000000000000000000 ) ) ;
#39337=B_SPLINE_CURVE_WITH_KNOTS ( 'NONE', 3,
 ( #56743, #2705, #37742, #62519, #3030, #41926 ),
 .UNSPECIFIED., .F., .F.,
 ( 4, 2, 4 ),
 ( 0.000000000000000000, 0.002307655110370371299, 0.004615310220740742597 ),
 .UNSPECIFIED. ) ;
#39344=EDGE_CURVE ( 'NONE', #1507, #48710, #46266, .T. ) ;
#39460=FACE_BOUND ( 'NONE', #6961, .T. ) ;
#39525=ORIENTED_EDGE ( 'NONE', *, *, #5485, .F. ) ;
#39557=LINE ( 'NONE', #34102, #27458 ) ;
#39562=AXIS2_PLACEMENT_3D ( 'NONE', #56818, #51980, #48088 ) ;
#39655=CARTESIAN_POINT ( 'NONE',  ( 0.5974722283283632196, -8.315303285985693904, -0.7026937717022971874 ) ) ;
#39690=CONICAL_SURFACE ( 'NONE', #54073, 10.39117206796836079, 1.221730476396047926 ) ;
#39707=CARTESIAN_POINT ( 'NONE',  ( 6.523606932381168733, 4.893847819346807348, -7.213065638943126245 ) ) ;
#39784=CARTESIAN_POINT ( 'NONE',  ( -7.908219015560238319, -3.084967917785936820, -7.795665562178438535 ) ) ;
#39788=EDGE_CURVE ( 'NONE', #26290, #37707, #38466, .T. ) ;
#39800=CARTESIAN_POINT ( 'NONE',  ( -1.306442393143578462, -8.377108146505394259, -7.792327460285862983 ) ) ;
#39804=EDGE_CURVE ( 'NONE', #21365, #28539, #12771, .T. ) ;
#39844=ORIENTED_EDGE ( 'NONE', *, *, #21206, .F. ) ;
#39878=CARTESIAN_POINT ( 'NONE',  ( 2.500000000000000444, 7.216878364870322748, -7.063244554130000630 ) ) ;
#39901=CARTESIAN_POINT ( 'NONE',  ( 0.000000000000000000, 0.000000000000000000, -9.999999999999998224 ) ) ;
#39918=CARTESIAN_POINT ( 'NONE',  ( 0.000000000000000000, 0.000000000000000000, 0.000000000000000000 ) ) ;
#40055=LINE ( 'NONE', #34275, #7964 ) ;
#40112=LINE ( 'NONE', #6043, #3955 ) ;
#40198=CARTESIAN_POINT ( 'NONE',  ( 0.000000000000000000, 0.000000000000000000, 0.000000000000000000 ) ) ;
#40224=ORIENTED_EDGE ( 'NONE', *, *, #28689, .T. ) ;
#40285=ORIENTED_EDGE ( 'NONE', *, *, #7942, .F. ) ;
#40313=CARTESIAN_POINT ( 'NONE',  ( -3.093533885184598375, -6.874201416485457017, -7.446478553994068328 ) ) ;
#40325=CARTESIAN_POINT ( 'NONE',  ( 7.894705354777835637, 0.7527931906242791849, -7.590204373988219011 ) ) ;
#40334=DIRECTION ( 'NONE',  ( 1.000000000000000000, 0.000000000000000000, 0.000000000000000000 ) ) ;
#40407=ORIENTED_EDGE ( 'NONE', *, *, #14577, .T. ) ;
#40421=EDGE_LOOP ( 'NONE', ( #28336, #23938, #38830, #61221 ) ) ;
#40464=VERTEX_POINT ( 'NONE', #13827 ) ;
#40496=CARTESIAN_POINT ( 'NONE',  ( -4.250000000000000000, 5.204748896376250699E-16, -10.00000000000000000 ) ) ;
#40543=VECTOR ( 'NONE', #51748, 1000.000000000000000 ) ;
#40708=DIRECTION ( 'NONE',  ( 1.000000000000000000, 0.000000000000000000, 0.000000000000000000 ) ) ;
#40713=ORIENTED_EDGE ( 'NONE', *, *, #57831, .F. ) ;
#40714=CARTESIAN_POINT ( 'NONE',  ( -3.750000000000004885, 6.495190528383289141, 0.000000000000000000 ) ) ;
#40834=CARTESIAN_POINT ( 'NONE',  ( 5.276498195232308674, -6.073236878017951312, -7.633618187056764981 ) ) ;
#40855=CARTESIAN_POINT ( 'NONE',  ( 0.000000000000000000, 0.000000000000000000, 0.000000000000000000 ) ) ;
#40865=DIRECTION ( 'NONE',  ( -1.000000000000000000, 0.000000000000000000, 0.000000000000000000 ) ) ;
#40875=EDGE_CURVE ( 'NONE', #4851, #60221, #46914, .T. ) ;
#40976=EDGE_CURVE ( 'NONE', #53762, #36069, #29493, .T. ) ;
#41057=EDGE_LOOP ( 'NONE', ( #22707, #51828, #6156, #17179, #60724 ) ) ;
#41148=CARTESIAN_POINT ( 'NONE',  ( 7.169303301815196150, -4.521054846639319003, -7.349897473155491134 ) ) ;
#41153=CARTESIAN_POINT ( 'NONE',  ( 0.6250000000000013323, 8.299410119600871383, -7.298562697733108173 ) ) ;
#41181=FACE_OUTER_BOUND ( 'NONE', #4347, .T. ) ;
#41263=CARTESIAN_POINT ( 'NONE',  ( 7.499999999997997158, -3.157198044624895061, -7.642795354507847527 ) ) ;
#41289=CARTESIAN_POINT ( 'NONE',  ( 7.500000000000000000, 4.330127018922190096, -10.00000000000000000 ) ) ;
#41293=VERTEX_POINT ( 'NONE', #8398 ) ;
#41336=B_SPLINE_CURVE_WITH_KNOTS ( 'NONE', 3,
 ( #26690, #46307, #12522, #27317, #2893, #22505 ),
 .UNSPECIFIED., .F., .F.,
 ( 4, 2, 4 ),
 ( 0.000000000000000000, 0.0004189869898913742632, 0.0008379739797827464665 ),
 .UNSPECIFIED. ) ;
#41339=CARTESIAN_POINT ( 'NONE',  ( -7.169303301815100227, 4.521054846639364300, -7.349897473154783256 ) ) ;
#41479=CARTESIAN_POINT ( 'NONE',  ( 7.922281120364393914, -4.573931137438282057, -8.047472243342932430 ) ) ;
#41569=B_SPLINE_CURVE_WITH_KNOTS ( 'NONE', 3,
 ( #55347, #352, #9985, #30885, #38, #30234 ),
 .UNSPECIFIED., .F., .F.,
 ( 4, 2, 4 ),
 ( -5.145455527297706927E-06, 0.0004153350442917481326, 0.0008358155441107939163 ),
 .UNSPECIFIED. ) ;
#41577=CARTESIAN_POINT ( 'NONE',  ( 7.894958282449824338, -1.603399432398892266, -7.593838100136980351 ) ) ;
#41602=CARTESIAN_POINT ( 'NONE',  ( 7.922281120364393914, 4.573931137438269623, -8.047472243342930653 ) ) ;
#41666=EDGE_CURVE ( 'NONE', #19824, #29058, #36631, .T. ) ;
#41786=CARTESIAN_POINT ( 'NONE',  ( 7.970070017554212960, -4.546953124339766283, -8.057670357645358550 ) ) ;
#41794=CARTESIAN_POINT ( 'NONE',  ( -7.500000000000000888, -1.443375672974068769, -7.063244554130002406 ) ) ;
#41885=DIRECTION ( 'NONE',  ( 1.000000000000000000, 0.000000000000000000, 0.000000000000000000 ) ) ;
#41926=CARTESIAN_POINT ( 'NONE',  ( 7.894787914004607998, 1.243647571710251278E-13, -7.591390474663425536 ) ) ;
#41934=AXIS2_PLACEMENT_3D ( 'NONE', #43285, #49050, #62616 ) ;
#42120=EDGE_CURVE ( 'NONE', #50022, #48710, #27236, .T. ) ;
#42168=CARTESIAN_POINT ( 'NONE',  ( -6.250000000000000888, 5.051814855409225480, -7.198902722707429369 ) ) ;
#42226=CARTESIAN_POINT ( 'NONE',  ( 4.250000000000000000, 0.000000000000000000, -10.00000000000000000 ) ) ;
#42306=CARTESIAN_POINT ( 'NONE',  ( -7.500000000000000888, -0.7512838658081441023, 1.307818870560639724E-15 ) ) ;
#42344=CIRCLE ( 'NONE', #1330, 4.250000000000000000 ) ;
#42394=ORIENTED_EDGE ( 'NONE', *, *, #7942, .T. ) ;
#42412=CARTESIAN_POINT ( 'NONE',  ( -7.500000000000000888, 3.639598441879742907, -0.7155132341745253921 ) ) ;
#42477=ADVANCED_FACE ( 'NONE', ( #32358 ), #1592, .T. ) ;
#42553=ADVANCED_FACE ( 'NONE', ( #14306 ), #17998, .F. ) ;
#42632=DIRECTION ( 'NONE',  ( -1.000000000000000000, 0.000000000000000000, 0.000000000000000000 ) ) ;
#42714=FILL_AREA_STYLE_COLOUR ( '', #57500 ) ;
#42806=EDGE_CURVE ( 'NONE', #727, #22078, #50316, .T. ) ;
#42999=CARTESIAN_POINT ( 'NONE',  ( -7.922281120364393914, 4.573931137438271399, -8.047472243342930653 ) ) ;
#43054=AXIS2_PLACEMENT_3D ( 'NONE', #62200, #38367, #13919 ) ;
#43139=DIRECTION ( 'NONE',  ( 0.5000000000000005551, -0.8660254037844383745, 0.000000000000000000 ) ) ;
#43185=ORIENTED_EDGE ( 'NONE', *, *, #44151, .F. ) ;
#43285=CARTESIAN_POINT ( 'NONE',  ( -7.500000000000000000, -4.330127018922198090, -10.00000000000000000 ) ) ;
#43296=CARTESIAN_POINT ( 'NONE',  ( -3.750000000000004885, 6.495190528383289141, 0.000000000000000000 ) ) ;
#43394=CARTESIAN_POINT ( 'NONE',  ( 0.000000000000000000, 0.000000000000000000, -9.226681596905677907 ) ) ;
#43425=B_SPLINE_CURVE_WITH_KNOTS ( 'NONE', 3,
 ( #15870, #15223, #20050, #770, #39655, #44807 ),
 .UNSPECIFIED., .F., .F.,
 ( 4, 2, 4 ),
 ( 0.004444412883774326306, 0.006655097293744431999, 0.008865781703714537693 ),
 .UNSPECIFIED. ) ;
#43428=ORIENTED_EDGE ( 'NONE', *, *, #59851, .T. ) ;
#43440=CARTESIAN_POINT ( 'NONE',  ( 5.000000000000000888, 0.000000000000000000, 0.000000000000000000 ) ) ;
#43520=PRODUCT_DEFINITION_SHAPE ( 'NONE', 'NONE',  #24902 ) ;
#43618=EDGE_CURVE ( 'NONE', #31318, #22078, #19477, .T. ) ;
#43646=DIRECTION ( 'NONE',  ( 1.000000000000000000, 0.000000000000000000, 0.000000000000000000 ) ) ;
#43672=ORIENTED_EDGE ( 'NONE', *, *, #49435, .F. ) ;
#43751=CARTESIAN_POINT ( 'NONE',  ( -7.640563834021360018E-16, -9.147862274876560562, -8.047472243342937759 ) ) ;
#43759=CARTESIAN_POINT ( 'NONE',  ( 4.999999999999999112, -5.773502691896267081, -7.063244554130005071 ) ) ;
#43778=ORIENTED_EDGE ( 'NONE', *, *, #42120, .T. ) ;
#43822=CONICAL_SURFACE ( 'NONE', #31541, 7.500000000000001776, 0.8594454914424796144 ) ;
#43893=CARTESIAN_POINT ( 'NONE',  ( 7.847095227763521308, 4.129731495738485414, -7.493596212620238894 ) ) ;
#43897=CARTESIAN_POINT ( 'NONE',  ( -7.500000000000000000, -4.330127018922198090, -7.422398894150034288 ) ) ;
#43916=EDGE_CURVE ( 'NONE', #14179, #50022, #50933, .T. ) ;
#44055=EDGE_CURVE ( 'NONE', #63519, #28539, #15130, .T. ) ;
#44103=DIRECTION ( 'NONE',  ( 0.000000000000000000, 0.000000000000000000, -1.000000000000000000 ) ) ;
#44151=EDGE_CURVE ( 'NONE', #40464, #22078, #50443, .T. ) ;
#44198=ORIENTED_EDGE ( 'NONE', *, *, #46840, .T. ) ;
#44218=CARTESIAN_POINT ( 'NONE',  ( 7.968863443239234456, 4.547634245050474533, -8.057411785091787237 ) ) ;
#44237=CARTESIAN_POINT ( 'NONE',  ( -7.894787914004607998, -0.7661396099416333261, -7.591390474663429089 ) ) ;
#44251=CARTESIAN_POINT ( 'NONE',  ( -5.088535779737005882, 5.722386535631696525, -7.491772860716161553 ) ) ;
#44347=DIRECTION ( 'NONE',  ( 1.224646799147353207E-16, 1.000000000000000000, 0.000000000000000000 ) ) ;
#44385=DIRECTION ( 'NONE',  ( 0.9396926207859143121, 1.150791560227857665E-16, -0.3420201433256525592 ) ) ;
#44395=CARTESIAN_POINT ( 'NONE',  ( 2.499999999999999112, -7.216878364870334295, -7.063244554130005959 ) ) ;
#44444=EDGE_CURVE ( 'NONE', #50022, #15732, #52703, .T. ) ;
#44484=CARTESIAN_POINT ( 'NONE',  ( -6.875000000000001776, -4.690970937165714894, -7.298562697733108173 ) ) ;
#44524=DIRECTION ( 'NONE',  ( -0.000000000000000000, -0.000000000000000000, 1.000000000000000000 ) ) ;
#44616=CARTESIAN_POINT ( 'NONE',  ( -7.499999999999650058, -0.7583608255766450812, -7.446489218764574147 ) ) ;
#44703=CARTESIAN_POINT ( 'NONE',  ( 7.500000000000000000, 4.330127018922190096, -7.422398894150032511 ) ) ;
#44774=DIRECTION ( 'NONE',  ( 1.000000000000000000, 0.000000000000000000, 0.000000000000000000 ) ) ;
#44787=CARTESIAN_POINT ( 'NONE',  ( -7.500000000000000000, -3.469446951953614189E-15, -6.991905250253751980 ) ) ;
#44807=CARTESIAN_POINT ( 'NONE',  ( -1.994931997373328159E-14, -8.660254037844390851, -1.000000000000000888 ) ) ;
#44826=CARTESIAN_POINT ( 'NONE',  ( 3.750000000000004441, -6.495190528383289141, 0.000000000000000000 ) ) ;
#44861=CARTESIAN_POINT ( 'NONE',  ( 7.777900015783946408, 4.169681370001526055, -7.928862157988300297 ) ) ;
#44898=EDGE_CURVE ( 'NONE', #14179, #60221, #24331, .T. ) ;
#44907=AXIS2_PLACEMENT_3D ( 'NONE', #36270, #33257, #13323 ) ;
#44960=CARTESIAN_POINT ( 'NONE',  ( -5.274401269815139237, -6.074457022762090652, -7.633824513837113912 ) ) ;
#44993=CARTESIAN_POINT ( 'NONE',  ( -7.640563834021360018E-16, -9.147862274876560562, -8.047472243342937759 ) ) ;
#45135=CARTESIAN_POINT ( 'NONE',  ( -7.777900015783941967, -4.169681370001537601, -7.928862157988302073 ) ) ;
#45228=ORIENTED_EDGE ( 'NONE', *, *, #31385, .F. ) ;
#45332=CARTESIAN_POINT ( 'NONE',  ( 7.500000000000000000, 4.330127018922190096, -10.00000000000000000 ) ) ;
#45359=CARTESIAN_POINT ( 'NONE',  ( 7.500000000000000888, 1.489914625144004523, -0.1187923833806749097 ) ) ;
#45407=ORIENTED_EDGE ( 'NONE', *, *, #25848, .F. ) ;
#45412=EDGE_LOOP ( 'NONE', ( #1785, #33850, #40713 ) ) ;
#45472=DIRECTION ( 'NONE',  ( -0.000000000000000000, -0.000000000000000000, 1.000000000000000000 ) ) ;
#45499=CARTESIAN_POINT ( 'NONE',  ( 7.499999999999999112, -1.443375672974070323, -7.063244554130001518 ) ) ;
#45509=CARTESIAN_POINT ( 'NONE',  ( 7.499999999999999112, -4.330127018922205195, -1.000000000000000888 ) ) ;
#45536=CARTESIAN_POINT ( 'NONE',  ( -7.779103221381273414, 4.168986698926021361, -7.929128246061903695 ) ) ;
#45656=CARTESIAN_POINT ( 'NONE',  ( -2.452879891156814818, -7.244083172395189507, -0.1007566405101857632 ) ) ;
#45668=CARTESIAN_POINT ( 'NONE',  ( 7.298354728637812983, -4.926141412639873707, -7.913704048099693189 ) ) ;
#45701=( BOUNDED_SURFACE ( )  B_SPLINE_SURFACE ( 3, 2, ( 
 ( #55449, #56407, #21983 ),
 ( #21673, #41263, #12332 ),
 ( #26804, #60911, #41577 ),
 ( #25851, #11364, #40325 ),
 ( #16833, #61230, #56080 ),
 ( #50614, #5923, #12000 ),
 ( #25531, #30675, #51264 ),
 ( #59963, #1747, #15886 ) ),
 .UNSPECIFIED., .F., .F., .F. ) 
 B_SPLINE_SURFACE_WITH_KNOTS ( ( 4, 2, 2, 4 ),
 ( 3, 3 ),
 ( 0.03850042371095789562, 0.04313406099830585649, 0.04545087964197984387, 0.04776769828565382431 ),
 ( 0.000000000000000000, 1.000000000000000000 ),
 .UNSPECIFIED. ) 
 GEOMETRIC_REPRESENTATION_ITEM ( )  RATIONAL_B_SPLINE_SURFACE ( (
 ( 1.000000000000000000, 0.8047781847388135734, 1.000000000000000000),
 ( 1.000000000000000000, 0.8123760230793541925, 1.000000000000000000),
 ( 1.000000000000000000, 0.8190653851695529619, 1.000000000000000000),
 ( 1.000000000000000000, 0.8191940386278896424, 1.000000000000000000),
 ( 1.000000000000000000, 0.8176096570055705337, 1.000000000000000000),
 ( 1.000000000000000000, 0.8122964723277524834, 1.000000000000000000),
 ( 1.000000000000000000, 0.8086312464132844324, 1.000000000000000000),
 ( 1.000000000000000000, 0.8047712192439641088, 1.000000000000000000) ) ) 
 REPRESENTATION_ITEM ( '' )  SURFACE ( )  );
#45774=CARTESIAN_POINT ( 'NONE',  ( -5.174575781537456010, -5.672711317431625488, -7.030005583190790830 ) ) ;
#45990=CARTESIAN_POINT ( 'NONE',  ( 4.999999999999999112, 5.773502691896256422, -7.063244554129997965 ) ) ;
#45993=CARTESIAN_POINT ( 'NONE',  ( 7.500000000000000888, 2.932633423934449812, -0.4709827563909316783 ) ) ;
#46091=CARTESIAN_POINT ( 'NONE',  ( -0.3875187462251565851, -8.436519985395204202, -7.781689322724289148 ) ) ;
#46206=PLANE ( 'NONE',  #24794 ) ;
#46266=B_SPLINE_CURVE_WITH_KNOTS ( 'NONE', 3,
 ( #19106, #38723, #5598, #25214, #53533, #44826 ),
 .UNSPECIFIED., .F., .F.,
 ( 4, 2, 4 ),
 ( 2.475503369227215526E-07, 0.002222330217055624568, 0.004444412883774326306 ),
 .UNSPECIFIED. ) ;
#46274=ORIENTED_EDGE ( 'NONE', *, *, #21206, .T. ) ;
#46303=B_SPLINE_CURVE_WITH_KNOTS ( 'NONE', 3,
 ( #15916, #10444, #35537, #45499, #15601, #60313, #10769, #26201, #21708 ),
 .UNSPECIFIED., .F., .F.,
 ( 4, 2, 1, 2, 4 ),
 ( 0.000000000000000000, 0.002165063509461097498, 0.004330127018922194995, 0.006495190528383292493, 0.008660254037844389990 ),
 .UNSPECIFIED. ) ;
#46307=CARTESIAN_POINT ( 'NONE',  ( 7.500000000000001776, 4.330127018922190985, -7.564338275809324941 ) ) ;
#46374=AXIS2_PLACEMENT_3D ( 'NONE', #18831, #4062, #33636 ) ;
#46400=CARTESIAN_POINT ( 'NONE',  ( 0.000000000000000000, 0.000000000000000000, -25.03750572909317285 ) ) ;
#46437=CARTESIAN_POINT ( 'NONE',  ( -8.285706625453232893E-17, -8.895730773063887042, -7.917997657324732153 ) ) ;
#46506=CARTESIAN_POINT ( 'NONE',  ( 0.000000000000000000, 0.000000000000000000, -25.03750572909317285 ) ) ;
#46529=DIRECTION ( 'NONE',  ( 0.000000000000000000, 0.000000000000000000, 1.000000000000000000 ) ) ;
#46623=CARTESIAN_POINT ( 'NONE',  ( 1.249327701954825010, -8.410337540182549532, -7.776713651265369620 ) ) ;
#46721=CARTESIAN_POINT ( 'NONE',  ( 7.908030677224553884, -3.059924800338349904, -7.792662696733364314 ) ) ;
#46840=EDGE_CURVE ( 'NONE', #6403, #24352, #11939, .T. ) ;
#46904=EDGE_LOOP ( 'NONE', ( #28613, #51097, #26862, #32345 ) ) ;
#46913=ORIENTED_EDGE ( 'NONE', *, *, #19975, .T. ) ;
#46914=LINE ( 'NONE', #32745, #47755 ) ;
#47143=DIRECTION ( 'NONE',  ( 0.000000000000000000, 0.000000000000000000, -1.000000000000000000 ) ) ;
#47172=CARTESIAN_POINT ( 'NONE',  ( 0.000000000000000000, 0.000000000000000000, -9.226681596905677907 ) ) ;
#47383=CARTESIAN_POINT ( 'NONE',  ( -14.99999999999998934, -1.734723475976807094E-15, 0.000000000000000000 ) ) ;
#47396=CARTESIAN_POINT ( 'NONE',  ( 0.6508621380849231031, 8.763657152406445050, -7.907633014911220393 ) ) ;
#47424=ORIENTED_EDGE ( 'NONE', *, *, #40976, .F. ) ;
#47439=ORIENTED_EDGE ( 'NONE', *, *, #40976, .T. ) ;
#47482=CARTESIAN_POINT ( 'NONE',  ( -7.549004593702450805, -4.358419834287835748, -7.700121441565821456 ) ) ;
#47507=CARTESIAN_POINT ( 'NONE',  ( 7.500000000000000000, -4.330127018922199866, -10.00000000000000000 ) ) ;
#47613=B_SPLINE_CURVE_WITH_KNOTS ( 'NONE', 3,
 ( #13845, #63383, #9025, #22886, #3892, #57617 ),
 .UNSPECIFIED., .F., .F.,
 ( 4, 2, 4 ),
 ( 0.004615310220740751271, 0.006918661718823357169, 0.009222013216905963068 ),
 .UNSPECIFIED. ) ;
#47646=CARTESIAN_POINT ( 'NONE',  ( 3.750000000000005329, 6.495190528383288253, 0.000000000000000000 ) ) ;
#47658=EDGE_CURVE ( 'NONE', #60221, #4973, #9691, .T. ) ;
#47665=CARTESIAN_POINT ( 'NONE',  ( 0.000000000000000000, 0.000000000000000000, 0.000000000000000000 ) ) ;
#47702=DIRECTION ( 'NONE',  ( -0.000000000000000000, -0.000000000000000000, 1.000000000000000000 ) ) ;
#47755=VECTOR ( 'NONE', #57208, 1000.000000000000000 ) ;
#47784=CARTESIAN_POINT ( 'NONE',  ( 0.000000000000000000, 0.000000000000000000, -9.974600000000000577 ) ) ;
#47790=VECTOR ( 'NONE', #20737, 1000.000000000000000 ) ;
#47835=AXIS2_PLACEMENT_3D ( 'NONE', #14485, #34, #33486 ) ;
#47860=CARTESIAN_POINT ( 'NONE',  ( -2.352990130084580066E-16, 8.660254037844390851, -10.00000000000000000 ) ) ;
#47880=AXIS2_PLACEMENT_3D ( 'NONE', #43394, #39197, #49175 ) ;
#47925=EDGE_CURVE ( 'NONE', #50923, #63287, #51122, .T. ) ;
#47933=AXIS2_PLACEMENT_3D ( 'NONE', #36284, #2827, #37232 ) ;
#48088=DIRECTION ( 'NONE',  ( -1.000000000000000000, 0.000000000000000000, 0.000000000000000000 ) ) ;
#48091=EDGE_LOOP ( 'NONE', ( #34240, #3036, #31364, #36795 ) ) ;
#48182=FACE_OUTER_BOUND ( 'NONE', #27221, .T. ) ;
#48215=CARTESIAN_POINT ( 'NONE',  ( 0.3483149870578491347, -8.861353789385031376, -7.493854785173814648 ) ) ;
#48237=PRODUCT_DEFINITION_FORMATION_WITH_SPECIFIED_SOURCE ( 'ANY', '', #19930, .NOT_KNOWN. ) ;
#48249=ORIENTED_EDGE ( 'NONE', *, *, #15362, .F. ) ;
#48257=CARTESIAN_POINT ( 'NONE',  ( -5.000000000000000888, 6.123233995736767268E-16, 0.000000000000000000 ) ) ;
#48368=ADVANCED_FACE ( 'NONE', ( #54524 ), #6917, .F. ) ;
#48497=LINE ( 'NONE', #52078, #5514 ) ;
#48710=VERTEX_POINT ( 'NONE', #3983 ) ;
#48711=UNCERTAINTY_MEASURE_WITH_UNIT (LENGTH_MEASURE( 1.000000000000000082E-05 ), #61097, 'distance_accuracy_value', 'NONE');
#48787=PLANE ( 'NONE',  #2229 ) ;
#48836=ORIENTED_EDGE ( 'NONE', *, *, #25660, .F. ) ;
#48859=DIRECTION ( 'NONE',  ( -1.000000000000000000, 1.224646799147354686E-16, 0.000000000000000000 ) ) ;
#48918=DIRECTION ( 'NONE',  ( 1.000000000000000000, 0.000000000000000000, 0.000000000000000000 ) ) ;
#49050=DIRECTION ( 'NONE',  ( -0.5000000000000008882, -0.8660254037844382635, 0.000000000000000000 ) ) ;
#49078=CARTESIAN_POINT ( 'NONE',  ( -5.112021521198522933, 5.708827036477257977, -7.069802615102034338 ) ) ;
#49126=CARTESIAN_POINT ( 'NONE',  ( -7.500000000000000000, 4.730921838224027454, -7.493596905200499592 ) ) ;
#49142=CARTESIAN_POINT ( 'NONE',  ( -3.750000000000007105, -6.495190528383289141, 0.000000000000000000 ) ) ;
#49175=DIRECTION ( 'NONE',  ( 1.000000000000000000, 0.000000000000000000, 0.000000000000000000 ) ) ;
#49290=VERTEX_POINT ( 'NONE', #7788 ) ;
#49314=CARTESIAN_POINT ( 'NONE',  ( -6.127431526422343306E-17, 9.147862274876549904, -8.047472243342932430 ) ) ;
#49319=CARTESIAN_POINT ( 'NONE',  ( -2.499999999999999556, -7.216878364870334295, -7.063244554130003294 ) ) ;
#49422=VERTEX_POINT ( 'NONE', #28649 ) ;
#49435=EDGE_CURVE ( 'NONE', #29985, #24352, #39557, .T. ) ;
#49449=CARTESIAN_POINT ( 'NONE',  ( -7.500000000000667910, 3.157052757790226316, -7.642767288269818771 ) ) ;
#49616=ORIENTED_EDGE ( 'NONE', *, *, #63433, .F. ) ;
#49723=CARTESIAN_POINT ( 'NONE',  ( 0.2779000157839532359, 8.820699686765054892, -7.928862157988302961 ) ) ;
#49850=ORIENTED_EDGE ( 'NONE', *, *, #41666, .T. ) ;
#49853=CARTESIAN_POINT ( 'NONE',  ( -5.000000000000000888, 6.123233995736767268E-16, -25.03750572909317285 ) ) ;
#49872=CARTESIAN_POINT ( 'NONE',  ( 5.000000000000001776, 6.123233995736768255E-16, -9.974600000000000577 ) ) ;
#50022=VERTEX_POINT ( 'NONE', #49142 ) ;
#50049=DIRECTION ( 'NONE',  ( -0.000000000000000000, -0.000000000000000000, 1.000000000000000000 ) ) ;
#50060=EDGE_CURVE ( 'NONE', #57220, #6403, #24374, .T. ) ;
#50087=MANIFOLD_SOLID_BREP ( 'EndChamfer', #57235 ) ;
#50162=ORIENTED_EDGE ( 'NONE', *, *, #50060, .T. ) ;
#50176=CARTESIAN_POINT ( 'NONE',  ( 1.250000000000000222, 7.938566201357357244, -7.198902722707428481 ) ) ;
#50204=CARTESIAN_POINT ( 'NONE',  ( 7.500000000000000000, -4.330127018922199866, -7.422398894150035176 ) ) ;
#50245=FACE_OUTER_BOUND ( 'NONE', #40421, .T. ) ;
#50299=CARTESIAN_POINT ( 'NONE',  ( 0.000000000000000000, 0.000000000000000000, -9.449444346342714240 ) ) ;
#50316=LINE ( 'NONE', #41289, #47790 ) ;
#50427=EDGE_CURVE ( 'NONE', #24352, #57225, #8951, .T. ) ;
#50443=B_SPLINE_CURVE_WITH_KNOTS ( 'NONE', 3,
 ( #6130, #26375, #35076, #45359, #26061, #5801, #45993, #1959, #34752, #54378 ),
 .UNSPECIFIED., .F., .F.,
 ( 4, 2, 2, 2, 4 ),
 ( 0.01051144076094935251, 0.01162027323572611265, 0.01272910571050287452, 0.01383793818527963640, 0.01494677066005639827 ),
 .UNSPECIFIED. ) ;
#50490=CARTESIAN_POINT ( 'NONE',  ( -0.5984201754795734907, -8.314755988442763979, -0.7022220667781372549 ) ) ;
#50507=CARTESIAN_POINT ( 'NONE',  ( -2.352990130084580066E-16, 8.660254037844390851, -7.422398894150034288 ) ) ;
#50545=ORIENTED_EDGE ( 'NONE', *, *, #39344, .F. ) ;
#50614=CARTESIAN_POINT ( 'NONE',  ( 7.500000000000000000, 3.160172554975063886, -7.231829826456836585 ) ) ;
#50658=CARTESIAN_POINT ( 'NONE',  ( 7.500000000000000000, -1.486698507076798847, -0.09861472150523931113 ) ) ;
#50703=EDGE_LOOP ( 'NONE', ( #25058, #32598, #59261, #13610 ) ) ;
#50923=VERTEX_POINT ( 'NONE', #3168 ) ;
#50933=CIRCLE ( 'NONE', #47835, 7.500000000000001776 ) ;
#51008=CARTESIAN_POINT ( 'NONE',  ( -7.848314987057850800, 4.129027267381560229, -7.493854785173809319 ) ) ;
#51097=ORIENTED_EDGE ( 'NONE', *, *, #5989, .T. ) ;
#51122=B_SPLINE_CURVE_WITH_KNOTS ( 'NONE', 3,
 ( #57794, #5010, #19157, #24630, #44237, #29121 ),
 .UNSPECIFIED., .F., .F.,
 ( 4, 2, 4 ),
 ( 0.000000000000000000, 0.002307655110370376069, 0.004615310220740751271 ),
 .UNSPECIFIED. ) ;
#51123=( NAMED_UNIT ( * ) PLANE_ANGLE_UNIT ( ) SI_UNIT ( $, .RADIAN. ) );
#51264=CARTESIAN_POINT ( 'NONE',  ( 7.915340744421234476, 3.857466640755322640, -7.913699667209310284 ) ) ;
#51273=CARTESIAN_POINT ( 'NONE',  ( -5.007715329123872641E-16, -8.660254037844399733, -7.422398894150038728 ) ) ;
#51290=CARTESIAN_POINT ( 'NONE',  ( 7.263825692932297962, 4.945657111639574666, -7.907570769506046204 ) ) ;
#51300=AXIS2_PLACEMENT_3D ( 'NONE', #18118, #47702, #33233 ) ;
#51303=CARTESIAN_POINT ( 'NONE',  ( 0.3306966981845720355, 8.469326210127405830, -7.349897473153450989 ) ) ;
#51430=VECTOR ( 'NONE', #3146, 1000.000000000000000 ) ;
#51443=ADVANCED_FACE ( 'NONE', ( #53769 ), #25293, .T. ) ;
#51459=CARTESIAN_POINT ( 'NONE',  ( 1.015826369459276846, -8.073766409988136772, -7.642786413614194529 ) ) ;
#51548=( BOUNDED_SURFACE ( )  B_SPLINE_SURFACE ( 3, 2, ( 
 ( #31828, #36978, #56606 ),
 ( #6754, #51459, #46623 ),
 ( #6445, #12523, #1627 ),
 ( #7077, #35706, #1318 ),
 ( #26054, #26691, #40834 ),
 ( #22185, #16721, #21228 ),
 ( #41148, #60161, #45668 ),
 ( #25737, #61115, #41786 ) ),
 .UNSPECIFIED., .F., .F., .F. ) 
 B_SPLINE_SURFACE_WITH_KNOTS ( ( 4, 2, 2, 4 ),
 ( 3, 3 ),
 ( 0.03861844051980971304, 0.04325213341840643266, 0.04556897986770479247, 0.04788582631700314535 ),
 ( 0.000000000000000000, 1.000000000000000000 ),
 .UNSPECIFIED. ) 
 GEOMETRIC_REPRESENTATION_ITEM ( )  RATIONAL_B_SPLINE_SURFACE ( (
 ( 1.000000000000000000, 0.8047781759831919013, 1.000000000000000000),
 ( 1.000000000000000000, 0.8123762462802479600, 1.000000000000000000),
 ( 1.000000000000000000, 0.8190659850620179983, 1.000000000000000000),
 ( 1.000000000000000000, 0.8191937571011910224, 1.000000000000000000),
 ( 1.000000000000000000, 0.8176092952781196521, 1.000000000000000000),
 ( 1.000000000000000000, 0.8122962088595743202, 1.000000000000000000),
 ( 1.000000000000000000, 0.8086311330828506172, 1.000000000000000000),
 ( 1.000000000000000000, 0.8047712282214323221, 1.000000000000000000) ) ) 
 REPRESENTATION_ITEM ( '' )  SURFACE ( )  );
#51674=DIRECTION ( 'NONE',  ( 1.000000000000000000, 0.000000000000000000, -0.000000000000000000 ) ) ;
#51675=ORIENTED_EDGE ( 'NONE', *, *, #3236, .T. ) ;
#51748=DIRECTION ( 'NONE',  ( 0.000000000000000000, 0.000000000000000000, 1.000000000000000000 ) ) ;
#51783=CARTESIAN_POINT ( 'NONE',  ( 4.250000000000000000, 0.000000000000000000, -0.5251556536572846712 ) ) ;
#51828=ORIENTED_EDGE ( 'NONE', *, *, #6876, .F. ) ;
#51875=ORIENTED_EDGE ( 'NONE', *, *, #28898, .T. ) ;
#51980=DIRECTION ( 'NONE',  ( 0.000000000000000000, 0.000000000000000000, -1.000000000000000000 ) ) ;
#52078=CARTESIAN_POINT ( 'NONE',  ( 5.000000000000001776, 6.123233995736768255E-16, -9.974600000000000577 ) ) ;
#52079=CIRCLE ( 'NONE', #17134, 0.7733184030943203169 ) ;
#52084=CARTESIAN_POINT ( 'NONE',  ( -7.500000000000000888, 3.988838049906426875, -0.8529248949437632232 ) ) ;
#52120=CONICAL_SURFACE ( 'NONE', #13084, 5.000000000000001776, 0.9599310885968795892 ) ;
#52126=( GEOMETRIC_REPRESENTATION_CONTEXT ( 3 ) GLOBAL_UNCERTAINTY_ASSIGNED_CONTEXT ( ( #8591 ) ) GLOBAL_UNIT_ASSIGNED_CONTEXT ( ( #9273, #58487, #19557 ) ) REPRESENTATION_CONTEXT ( 'NONE', 'WORKASPACE' ) );
#52175=LINE ( 'NONE', #18068, #1118 ) ;
#52301=CIRCLE ( 'NONE', #51300, 4.250000000000000000 ) ;
#52347=ORIENTED_EDGE ( 'NONE', *, *, #5823, .T. ) ;
#52368=ADVANCED_FACE ( 'NONE', ( #41181 ), #39690, .T. ) ;
#52474=ORIENTED_EDGE ( 'NONE', *, *, #22100, .F. ) ;
#52531=CARTESIAN_POINT ( 'NONE',  ( -6.255257926720099353E-16, -8.716842316802392077, -7.700127545397295492 ) ) ;
#52622=DIRECTION ( 'NONE',  ( -1.000000000000000000, 0.000000000000000000, 0.000000000000000000 ) ) ;
#52684=CARTESIAN_POINT ( 'NONE',  ( -7.500000000000000000, 4.330127018922191873, -10.00000000000000000 ) ) ;
#52703=B_SPLINE_CURVE_WITH_KNOTS ( 'NONE', 3,
 ( #35581, #54564, #60358, #25610, #11125, #55535 ),
 .UNSPECIFIED., .F., .F.,
 ( 4, 2, 4 ),
 ( 0.004444412883774350592, 0.006655097293744440673, 0.008865781703714530754 ),
 .UNSPECIFIED. ) ;
#52782=ORIENTED_EDGE ( 'NONE', *, *, #44898, .T. ) ;
#52805=PLANE ( 'NONE',  #10314 ) ;
#52915=ORIENTED_EDGE ( 'NONE', *, *, #28898, .F. ) ;
#53222=CARTESIAN_POINT ( 'NONE',  ( -5.134616530693477992E-16, 8.895721644649725590, -7.917989418073275942 ) ) ;
#53241=ORIENTED_EDGE ( 'NONE', *, *, #43618, .F. ) ;
#53327=PLANE ( 'NONE',  #13733 ) ;
#53450=B_SPLINE_CURVE_WITH_KNOTS ( 'NONE', 3,
 ( #56767, #56453, #13001, #61909, #60961, #17829 ),
 .UNSPECIFIED., .F., .F.,
 ( 4, 2, 4 ),
 ( 0.004444412883774334112, 0.006655097293744431999, 0.008865781703714530754 ),
 .UNSPECIFIED. ) ;
#53533=CARTESIAN_POINT ( 'NONE',  ( 4.406842699996126989, -6.115962218725295330, -6.291760732204942919E-15 ) ) ;
#53565=CARTESIAN_POINT ( 'NONE',  ( 5.147825380264231754, 5.688155668806028409, -7.450218641347809090 ) ) ;
#53598=CARTESIAN_POINT ( 'NONE',  ( -1.249327701954873415, 8.410337540189265937, -7.776713651267812999 ) ) ;
#53633=ORIENTED_EDGE ( 'NONE', *, *, #43618, .T. ) ;
#53640=CARTESIAN_POINT ( 'NONE',  ( -7.897827455343210623, -1.533134349199909208, -7.633632140068262295 ) ) ;
#53758=AXIS2_PLACEMENT_3D ( 'NONE', #40198, #9965, #15756 ) ;
#53762=VERTEX_POINT ( 'NONE', #49314 ) ;
#53769=FACE_OUTER_BOUND ( 'NONE', #3044, .T. ) ;
#53971=DIRECTION ( 'NONE',  ( -0.000000000000000000, -0.000000000000000000, 1.000000000000000000 ) ) ;
#54041=CARTESIAN_POINT ( 'NONE',  ( 7.264118654998712898, -4.945491722146229563, -7.907633014911220393 ) ) ;
#54073=AXIS2_PLACEMENT_3D ( 'NONE', #21258, #59551, #40865 ) ;
#54151=CARTESIAN_POINT ( 'NONE',  ( -2.352990130084580066E-16, 8.660254037844390851, -7.422398894150034288 ) ) ;
#54171=TOROIDAL_SURFACE ( 'NONE', #25397, 10.12668159690567649, 0.7733184030943209830 ) ;
#54256=CIRCLE ( 'NONE', #2956, 10.39117206796836079 ) ;
#54268=ORIENTED_EDGE ( 'NONE', *, *, #1265, .T. ) ;
#54378=CARTESIAN_POINT ( 'NONE',  ( 7.500000000000000000, 4.330127018922199866, -1.000000000000000888 ) ) ;
#54524=FACE_OUTER_BOUND ( 'NONE', #13914, .T. ) ;
#54564=CARTESIAN_POINT ( 'NONE',  ( -4.403473400622099909, -6.117907484625868975, -5.839445138371144960E-15 ) ) ;
#54574=ORIENTED_EDGE ( 'NONE', *, *, #9536, .T. ) ;
#54614=ORIENTED_EDGE ( 'NONE', *, *, #9536, .F. ) ;
#54627=ADVANCED_FACE ( 'NONE', ( #36045 ), #43822, .T. ) ;
#54722=CARTESIAN_POINT ( 'NONE',  ( 7.808623696107892975, -4.508310992946673146, -7.999704684617491068 ) ) ;
#54900=CARTESIAN_POINT ( 'NONE',  ( 0.000000000000000000, 0.000000000000000000, 0.000000000000000000 ) ) ;
#54917=CARTESIAN_POINT ( 'NONE',  ( -7.499999999999999112, -4.652405105468739421, -7.929127756970856034 ) ) ;
#54996=ORIENTED_EDGE ( 'NONE', *, *, #43916, .F. ) ;
#55274=CARTESIAN_POINT ( 'NONE',  ( 7.500000000000000000, 4.330127018922190096, -7.422398894150032511 ) ) ;
#55347=CARTESIAN_POINT ( 'NONE',  ( -7.922281120364393914, 4.573931137438271399, -8.047472243342930653 ) ) ;
#55366=ORIENTED_EDGE ( 'NONE', *, *, #1987, .F. ) ;
#55414=CARTESIAN_POINT ( 'NONE',  ( -7.499999999999999112, 1.443375672974061219, -7.063244554130000630 ) ) ;
#55449=CARTESIAN_POINT ( 'NONE',  ( 7.500000000000000000, -4.730916290271713898, -7.493595886788494198 ) ) ;
#55468=ORIENTED_EDGE ( 'NONE', *, *, #9964, .F. ) ;
#55489=CARTESIAN_POINT ( 'NONE',  ( 0.3875187462248268488, 8.436519985393664101, -7.781689322726965230 ) ) ;
#55492=ADVANCED_FACE ( 'NONE', ( #50245 ), #1699, .F. ) ;
#55535=CARTESIAN_POINT ( 'NONE',  ( -7.500000000000000000, -4.330127018922199866, -1.000000000000000888 ) ) ;
#55749=CARTESIAN_POINT ( 'NONE',  ( -1.060314165522979968, -8.048081368954337123, -7.659344964963557878 ) ) ;
#55784=DIRECTION ( 'NONE',  ( -0.000000000000000000, -0.000000000000000000, 1.000000000000000000 ) ) ;
#55794=ADVANCED_FACE ( 'NONE', ( #14630 ), #52120, .F. ) ;
#55835=CARTESIAN_POINT ( 'NONE',  ( -7.112481253775184697, 4.553861071372892866, -7.781689322728085223 ) ) ;
#55872=ORIENTED_EDGE ( 'NONE', *, *, #15780, .F. ) ;
#56069=CARTESIAN_POINT ( 'NONE',  ( -7.968863443239230016, -4.547634245050486079, -8.057411785091789014 ) ) ;
#56080=CARTESIAN_POINT ( 'NONE',  ( 7.897825807688775512, 1.532833846124499910, -7.633607627188418121 ) ) ;
#56100=DIRECTION ( 'NONE',  ( 1.000000000000000000, 0.000000000000000000, 0.000000000000000000 ) ) ;
#56105=CARTESIAN_POINT ( 'NONE',  ( 3.280815508853482498, 7.221948645665444921, -7.591546097228400569 ) ) ;
#56117=CARTESIAN_POINT ( 'NONE',  ( -0.2791032213812780771, 8.821394357840562250, -7.929128246061909024 ) ) ;
#56280=CARTESIAN_POINT ( 'NONE',  ( -7.500000000000000888, 2.575910028905295857, -0.3641256808890092067 ) ) ;
#56287=EDGE_LOOP ( 'NONE', ( #4112, #61901, #54268, #25466, #52782 ) ) ;
#56407=CARTESIAN_POINT ( 'NONE',  ( 7.500000000000000888, -4.651016565836964212, -7.928861822685564498 ) ) ;
#56453=CARTESIAN_POINT ( 'NONE',  ( -3.096526599377909417, 6.872473572140716414, 1.143494478793305063E-15 ) ) ;
#56537=VECTOR ( 'NONE', #38331, 1000.000000000000114 ) ;
#56606=CARTESIAN_POINT ( 'NONE',  ( -0.04606493828583551470, -9.175055303659563677, -8.057411785091794343 ) ) ;
#56699=DIRECTION ( 'NONE',  ( 1.000000000000000000, 0.000000000000000000, 0.000000000000000000 ) ) ;
#56743=CARTESIAN_POINT ( 'NONE',  ( 7.922281120364393914, 4.573931137438269623, -8.047472243342930653 ) ) ;
#56767=CARTESIAN_POINT ( 'NONE',  ( -3.750000000000004885, 6.495190528383289141, 0.000000000000000000 ) ) ;
#56806=FACE_OUTER_BOUND ( 'NONE', #4051, .T. ) ;
#56815=FACE_OUTER_BOUND ( 'NONE', #8235, .T. ) ;
#56818=CARTESIAN_POINT ( 'NONE',  ( 0.000000000000000000, 0.000000000000000000, 0.000000000000000000 ) ) ;
#56833=FACE_OUTER_BOUND ( 'NONE', #13126, .T. ) ;
#56901=( NAMED_UNIT ( * ) SI_UNIT ( $, .STERADIAN. ) SOLID_ANGLE_UNIT ( ) );
#56965=FACE_OUTER_BOUND ( 'NONE', #45412, .T. ) ;
#57040=ADVANCED_BREP_SHAPE_REPRESENTATION ( '', ( #50087, #43054 ), #24596 ) ;
#57182=EDGE_LOOP ( 'NONE', ( #25153, #4353, #46913, #46274, #23418, #43778 ) ) ;
#57208=DIRECTION ( 'NONE',  ( 0.000000000000000000, 0.000000000000000000, 1.000000000000000000 ) ) ;
#57220=VERTEX_POINT ( 'NONE', #12210 ) ;
#57225=VERTEX_POINT ( 'NONE', #21868 ) ;
#57229=DIRECTION ( 'NONE',  ( 0.8191520442889907994, 1.003171929053523514E-16, -0.5735764363510474917 ) ) ;
#57231=MECHANICAL_DESIGN_GEOMETRIC_PRESENTATION_REPRESENTATION('',(#36696),#52126);
#57235=CLOSED_SHELL ( 'NONE', ( #28326, #55794, #38821, #10682, #4101, #28285, #55492, #36348, #34257, #17402, #28615, #31026, #25223, #12915, #33049, #1713, #52368, #832, #54627, #42477, #5262, #24842, #51443, #17871, #57380, #36605, #19620, #21731, #48368, #42553, #63429, #61740 ) ) ;
#57321=AXIS2_PLACEMENT_3D ( 'NONE', #39901, #20629, #48918 ) ;
#57380=ADVANCED_FACE ( 'NONE', ( #11250 ), #51548, .F. ) ;
#57500=COLOUR_RGB ( '',1.000000000000000000, 0.9490196078431372140, 0.9098039215686274384 ) ;
#57525=DIRECTION ( 'NONE',  ( -1.000000000000000000, 0.000000000000000000, 0.000000000000000000 ) ) ;
#57617=CARTESIAN_POINT ( 'NONE',  ( -7.922281120364393914, 4.573931137438271399, -8.047472243342930653 ) ) ;
#57685=CARTESIAN_POINT ( 'NONE',  ( -7.500000000000000000, -4.330127018922198090, -7.422398894150034288 ) ) ;
#57696=( BOUNDED_SURFACE ( )  B_SPLINE_SURFACE ( 3, 2, ( 
 ( #60586, #45135, #56069 ),
 ( #1099, #26477, #26155 ),
 ( #45774, #20708, #1733 ),
 ( #16820, #40313, #26793 ),
 ( #36439, #59951, #6228 ),
 ( #36127, #55749, #11666 ),
 ( #31285, #46091, #2051 ),
 ( #48215, #33125, #24098 ) ),
 .UNSPECIFIED., .F., .F., .F. ) 
 B_SPLINE_SURFACE_WITH_KNOTS ( ( 4, 2, 2, 4 ),
 ( 3, 3 ),
 ( 0.03861844051980971304, 0.04325213341840642572, 0.04556897986770477860, 0.04788582631700313841 ),
 ( 0.000000000000000000, 1.000000000000000000 ),
 .UNSPECIFIED. ) 
 GEOMETRIC_REPRESENTATION_ITEM ( )  RATIONAL_B_SPLINE_SURFACE ( (
 ( 1.000000000000000000, 0.8047781759831923454, 1.000000000000000000),
 ( 1.000000000000000000, 0.8123762462805160789, 1.000000000000000000),
 ( 1.000000000000000000, 0.8190659850616602844, 1.000000000000000000),
 ( 1.000000000000000000, 0.8191937571013702124, 1.000000000000000000),
 ( 1.000000000000000000, 0.8176092952780309453, 1.000000000000000000),
 ( 1.000000000000000000, 0.8122962088596628050, 1.000000000000000000),
 ( 1.000000000000000000, 0.8086311330827828936, 1.000000000000000000),
 ( 1.000000000000000000, 0.8047712282214327661, 1.000000000000000000) ) ) 
 REPRESENTATION_ITEM ( '' )  SURFACE ( )  );
#57794=CARTESIAN_POINT ( 'NONE',  ( -7.922281120364393914, -4.573931137438277617, -8.047472243342932430 ) ) ;
#57831=EDGE_CURVE ( 'NONE', #4973, #21052, #53450, .T. ) ;
#57845=( NAMED_UNIT ( * ) SI_UNIT ( $, .STERADIAN. ) SOLID_ANGLE_UNIT ( ) );
#58294=DIRECTION ( 'NONE',  ( 0.000000000000000000, 0.000000000000000000, -1.000000000000000000 ) ) ;
#58448=B_SPLINE_CURVE_WITH_KNOTS ( 'NONE', 3,
 ( #7598, #12087, #27205, #31710, #7283, #32344, #42306, #37486 ),
 .UNSPECIFIED., .F., .F.,
 ( 4, 2, 2, 4 ),
 ( 0.006061689441712453386, 0.007174127271521677299, 0.008286565101330901212, 0.01051144076094934904 ),
 .UNSPECIFIED. ) ;
#58471=DIRECTION ( 'NONE',  ( 0.000000000000000000, 0.000000000000000000, 1.000000000000000000 ) ) ;
#58487=( NAMED_UNIT ( * ) PLANE_ANGLE_UNIT ( ) SI_UNIT ( $, .RADIAN. ) );
#58598=DIRECTION ( 'NONE',  ( 0.000000000000000000, 0.000000000000000000, 1.000000000000000000 ) ) ;
#58659=CARTESIAN_POINT ( 'NONE',  ( 7.500000000000000000, -4.330127018922199866, -7.422398894150035176 ) ) ;
#58732=DIRECTION ( 'NONE',  ( 0.000000000000000000, 0.000000000000000000, -1.000000000000000000 ) ) ;
#58738=CARTESIAN_POINT ( 'NONE',  ( -4.406466114815342117, 6.116179640280717145, -7.446478553995464544 ) ) ;
#58792=CARTESIAN_POINT ( 'NONE',  ( -6.602753909532903975, -5.319290460493544259, -7.792447862505333056 ) ) ;
#58850=ORIENTED_EDGE ( 'NONE', *, *, #5485, .T. ) ;
#58876=CARTESIAN_POINT ( 'NONE',  ( 6.250000000000000000, -5.051814855409237026, -7.198902722707430257 ) ) ;
#58877=ORIENTED_EDGE ( 'NONE', *, *, #11751, .T. ) ;
#58906=CARTESIAN_POINT ( 'NONE',  ( -4.250000000000000000, 5.204748896376250699E-16, -9.449444346342714240 ) ) ;
#58910=CARTESIAN_POINT ( 'NONE',  ( -10.39117206796836079, 0.000000000000000000, -8.499999999999998224 ) ) ;
#59022=CARTESIAN_POINT ( 'NONE',  ( 3.295171437449806451, 7.213553046161976567, -7.590212325761626744 ) ) ;
#59030=FACE_OUTER_BOUND ( 'NONE', #27901, .T. ) ;
#59062=CARTESIAN_POINT ( 'NONE',  ( -0.9763930676156993282, 8.096533237421580154, -7.213065638943424673 ) ) ;
#59095=FACE_OUTER_BOUND ( 'NONE', #274, .T. ) ;
#59200=CARTESIAN_POINT ( 'NONE',  ( 4.613983237546155358, -6.452243898629820507, -7.591546097228409451 ) ) ;
#59261=ORIENTED_EDGE ( 'NONE', *, *, #20933, .T. ) ;
#59347=CARTESIAN_POINT ( 'NONE',  ( 5.174575781541291164, 5.672711317429402378, -7.030005583190089169 ) ) ;
#59352=CARTESIAN_POINT ( 'NONE',  ( 3.750000000000005329, 6.495190528383288253, 0.000000000000000000 ) ) ;
#59434=CARTESIAN_POINT ( 'NONE',  ( -7.500000000000000000, 4.330127018922191873, -0.9999999999999970024 ) ) ;
#59446=EDGE_LOOP ( 'NONE', ( #42394, #54614, #49616, #29399, #55366 ) ) ;
#59513=EDGE_CURVE ( 'NONE', #21052, #31318, #9577, .T. ) ;
#59550=CARTESIAN_POINT ( 'NONE',  ( 7.703928834700296768, -4.447865386531944409, -7.917997657324732153 ) ) ;
#59551=DIRECTION ( 'NONE',  ( 0.000000000000000000, 0.000000000000000000, -1.000000000000000000 ) ) ;
#59566=DIRECTION ( 'NONE',  ( 1.000000000000000000, 0.000000000000000000, 0.000000000000000000 ) ) ;
#59602=AXIS2_PLACEMENT_3D ( 'NONE', #22775, #62010, #13735 ) ;
#59605=CARTESIAN_POINT ( 'NONE',  ( -7.500000000000000000, -2.886751345948133984, -7.198902722707428481 ) ) ;
#59650=AXIS2_PLACEMENT_3D ( 'NONE', #2665, #22286, #41885 ) ;
#59851=EDGE_CURVE ( 'NONE', #57225, #24352, #54256, .T. ) ;
#59938=CARTESIAN_POINT ( 'NONE',  ( 0.000000000000000000, 0.000000000000000000, -10.00000000000000000 ) ) ;
#59951=CARTESIAN_POINT ( 'NONE',  ( -2.411464220262952818, -7.267994521134228059, -7.491772860715828486 ) ) ;
#59963=CARTESIAN_POINT ( 'NONE',  ( 7.500000000000000000, 4.732328341851997244, -7.493855119309152713 ) ) ;
#59982=ORIENTED_EDGE ( 'NONE', *, *, #60236, .F. ) ;
#59995=CARTESIAN_POINT ( 'NONE',  ( 2.411464220263165092, 7.267994521134541586, -7.491772860716163329 ) ) ;
#60030=CARTESIAN_POINT ( 'NONE',  ( -6.625705691649848461, 5.306270977113102916, -7.795653906409009792 ) ) ;
#60161=CARTESIAN_POINT ( 'NONE',  ( 7.112481253774308954, -4.553861071371678726, -7.781689322728511549 ) ) ;
#60198=B_SPLINE_CURVE_WITH_KNOTS ( 'NONE', 3,
 ( #50204, #31535, #36055, #59550, #54722, #26083 ),
 .UNSPECIFIED., .F., .F.,
 ( 4, 2, 4 ),
 ( 0.000000000000000000, 0.0004189869898913725285, 0.0008379739797827450570 ),
 .UNSPECIFIED. ) ;
#60221=VERTEX_POINT ( 'NONE', #59434 ) ;
#60230=ORIENTED_EDGE ( 'NONE', *, *, #60236, .T. ) ;
#60236=EDGE_CURVE ( 'NONE', #22221, #21052, #40112, .T. ) ;
#60284=DIRECTION ( 'NONE',  ( -1.000000000000000000, 0.000000000000000000, 0.000000000000000000 ) ) ;
#60287=FACE_BOUND ( 'NONE', #28842, .T. ) ;
#60313=CARTESIAN_POINT ( 'NONE',  ( 7.500000000000000888, 1.443375672974060109, -7.063244554130000630 ) ) ;
#60324=CARTESIAN_POINT ( 'NONE',  ( 7.500000000000000888, -3.640541674360523228, -0.7158139487964624292 ) ) ;
#60358=CARTESIAN_POINT ( 'NONE',  ( -5.040301471719076609, -5.750234626350520628, -0.09933465333851741741 ) ) ;
#60552=DIRECTION ( 'NONE',  ( 0.000000000000000000, 0.000000000000000000, 1.000000000000000000 ) ) ;
#60586=CARTESIAN_POINT ( 'NONE',  ( -7.847095227763516867, -4.129731495738496960, -7.493596212620239783 ) ) ;
#60637=CARTESIAN_POINT ( 'NONE',  ( 0.6169862416622686752, 8.783631307150953305, -7.913704048099833521 ) ) ;
#60724=ORIENTED_EDGE ( 'NONE', *, *, #47925, .F. ) ;
#60911=CARTESIAN_POINT ( 'NONE',  ( 7.499999999999999112, -1.614186302720606481, -7.450236204328171574 ) ) ;
#60951=ORIENTED_EDGE ( 'NONE', *, *, #5182, .F. ) ;
#60953=CARTESIAN_POINT ( 'NONE',  ( 2.621328321948289020, 7.606199919103058704, -7.633618187056857352 ) ) ;
#60961=CARTESIAN_POINT ( 'NONE',  ( -0.5974722283283655511, 8.315303285985683246, -0.7026937717022859742 ) ) ;
#61097=( LENGTH_UNIT ( ) NAMED_UNIT ( * ) SI_UNIT ( .MILLI., .METRE. ) );
#61115=CARTESIAN_POINT ( 'NONE',  ( 7.779103221381273414, -4.168986698926031131, -7.929128246061905472 ) ) ;
#61175=CARTESIAN_POINT ( 'NONE',  ( -6.874999999999995559, 4.690970937165706900, -7.298562697733101068 ) ) ;
#61211=LINE ( 'NONE', #61850, #12356 ) ;
#61219=AXIS2_PLACEMENT_3D ( 'NONE', #45332, #26038, #21851 ) ;
#61221=ORIENTED_EDGE ( 'NONE', *, *, #29373, .F. ) ;
#61230=CARTESIAN_POINT ( 'NONE',  ( 7.500000000000000000, 1.545478204151513157, -7.491761935628701075 ) ) ;
#61330=ORIENTED_EDGE ( 'NONE', *, *, #2418, .T. ) ;
#61363=AXIS2_PLACEMENT_3D ( 'NONE', #28261, #53971, #8964 ) ;
#61371=LINE ( 'NONE', #47507, #51430 ) ;
#61438=CARTESIAN_POINT ( 'NONE',  ( -7.500000000000000000, -4.330127018922198090, -7.422398894150034288 ) ) ;
#61441=CARTESIAN_POINT ( 'NONE',  ( 10.12668159690567649, 0.000000000000000000, -9.226681596905677907 ) ) ;
#61495=ORIENTED_EDGE ( 'NONE', *, *, #26301, .T. ) ;
#61576=CARTESIAN_POINT ( 'NONE',  ( 1.206569728928466700, 7.963640680051486953, -0.4524126574264497602 ) ) ;
#61582=AXIS2_PLACEMENT_3D ( 'NONE', #8168, #32279, #3968 ) ;
#61740=ADVANCED_FACE ( 'NONE', ( #15643 ), #35259, .F. ) ;
#61804=CARTESIAN_POINT ( 'NONE',  ( -7.500000000000000000, 4.330127018922191873, -7.422398894150032511 ) ) ;
#61842=CARTESIAN_POINT ( 'NONE',  ( -5.007715329123872641E-16, -8.660254037844399733, -10.00000000000000000 ) ) ;
#61850=CARTESIAN_POINT ( 'NONE',  ( 4.174999999999999822, 0.000000000000000000, -0.5776712190230133270 ) ) ;
#61887=FACE_OUTER_BOUND ( 'NONE', #32933, .T. ) ;
#61895=CARTESIAN_POINT ( 'NONE',  ( 2.452879891156805492, 7.244083172395185954, -0.1007566405101774504 ) ) ;
#61901=ORIENTED_EDGE ( 'NONE', *, *, #6876, .T. ) ;
#61909=CARTESIAN_POINT ( 'NONE',  ( -1.211595439868048629, 7.960739084487649109, -0.4504974108211966533 ) ) ;
#62002=ORIENTED_EDGE ( 'NONE', *, *, #9441, .F. ) ;
#62010=DIRECTION ( 'NONE',  ( -0.000000000000000000, -0.000000000000000000, -1.000000000000000000 ) ) ;
#62200=CARTESIAN_POINT ( 'NONE',  ( 0.000000000000000000, 0.000000000000000000, 0.000000000000000000 ) ) ;
#62251=DIRECTION ( 'NONE',  ( -0.8191520442889907994, 0.000000000000000000, -0.5735764363510474917 ) ) ;
#62357=SURFACE_STYLE_FILL_AREA ( #62675 ) ;
#62370=CONICAL_SURFACE ( 'NONE', #47933, 7.500000000000001776, 0.8594454914424796144 ) ;
#62480=EDGE_CURVE ( 'NONE', #49290, #32825, #32579, .T. ) ;
#62489=EDGE_LOOP ( 'NONE', ( #52915, #6187, #4969, #43185, #45228 ) ) ;
#62519=CARTESIAN_POINT ( 'NONE',  ( 7.897836333153806621, 1.530409084195003988, -7.633857274177628049 ) ) ;
#62520=ORIENTED_EDGE ( 'NONE', *, *, #18800, .F. ) ;
#62548=VECTOR ( 'NONE', #2685, 1000.000000000000000 ) ;
#62588=CARTESIAN_POINT ( 'NONE',  ( -7.500000000000001776, 0.000000000000000000, 0.000000000000000000 ) ) ;
#62589=DIRECTION ( 'NONE',  ( 0.000000000000000000, 0.000000000000000000, -1.000000000000000000 ) ) ;
#62616=DIRECTION ( 'NONE',  ( 0.8660254037844381525, -0.5000000000000007772, 0.000000000000000000 ) ) ;
#62644=CARTESIAN_POINT ( 'NONE',  ( -0.6511518506208974211, 8.763486134561267349, -7.907570769506047981 ) ) ;
#62648=EDGE_CURVE ( 'NONE', #63287, #57225, #4882, .T. ) ;
#62675=FILL_AREA_STYLE ('',( #42714 ) ) ;
#62733=ORIENTED_EDGE ( 'NONE', *, *, #57831, .T. ) ;
#62815=CONICAL_SURFACE ( 'NONE', #36086, 7.500000000000001776, 0.8594454914424796144 ) ;
#62906=ORIENTED_EDGE ( 'NONE', *, *, #50060, .F. ) ;
#63084=CARTESIAN_POINT ( 'NONE',  ( 0.6511518506208960888, -8.763486134561278007, -7.907570769506051533 ) ) ;
#63104=DIRECTION ( 'NONE',  ( 1.000000000000000000, 0.000000000000000000, 0.000000000000000000 ) ) ;
#63192=AXIS2_PLACEMENT_3D ( 'NONE', #54900, #4419, #43646 ) ;
#63287=VERTEX_POINT ( 'NONE', #7739 ) ;
#63299=LINE ( 'NONE', #19218, #15759 ) ;
#63383=CARTESIAN_POINT ( 'NONE',  ( -7.894787914004607998, 0.7647108141804108694, -7.591390474663421095 ) ) ;
#63429=ADVANCED_FACE ( 'NONE', ( #61887 ), #33827, .F. ) ;
#63433=EDGE_CURVE ( 'NONE', #36069, #29985, #39337, .T. ) ;
#63519=VERTEX_POINT ( 'NONE', #7847 ) ;
#63542=CARTESIAN_POINT ( 'NONE',  ( 3.080866544135574259, 6.881514909250401324, -7.026396753507782478 ) ) ;
#63602=DIRECTION ( 'NONE',  ( 0.000000000000000000, 0.000000000000000000, 1.000000000000000000 ) ) ;
#63608=EDGE_CURVE ( 'NONE', #19824, #49290, #52301, .T. ) ;
#63631=DIRECTION ( 'NONE',  ( -0.000000000000000000, -0.000000000000000000, -1.000000000000000000 ) ) ;
#63652=ORIENTED_EDGE ( 'NONE', *, *, #39344, .T. ) ;
#63713=COLOUR_RGB('Black',0.12,0.14,0.17);
#63714=FILL_AREA_STYLE_COLOUR('',#63713);
#63715=FILL_AREA_STYLE('',(#63714));
#63716=SURFACE_STYLE_FILL_AREA(#63715);
#63717=SURFACE_SIDE_STYLE('',(#63716));
#63718=SURFACE_STYLE_USAGE(.BOTH.,#63717);
#63719=PRESENTATION_STYLE_ASSIGNMENT((#63718));
ENDSEC;
END-ISO-10303-21;
